ISO-10303-21;
HEADER;
FILE_DESCRIPTION (('STEP AP214'),
    '1' );
FILE_NAME ('lid.step',
    '2026-10-26T05:17:54',
    ( '' ),
    ( '' ),
    'SwSTEP 2.0',
    'SolidWorks 2026',
    '' );
FILE_SCHEMA (( 'AUTOMOTIVE_DESIGN' ));
ENDSEC;

DATA;
#4=CARTESIAN_POINT ( 'NONE',  ( 35.00000000000000000, 126.3079067962035822, 4.296875000614517326 ) ) ;
#27=CARTESIAN_POINT ( 'NONE',  ( 33.50000000000000711, 79.80000000000001137, 8.000000000000000000 ) ) ;
#44=CARTESIAN_POINT ( 'NONE',  ( 50.72178482187501203, 62.76906990284730625, 4.503125000614517148 ) ) ;
#49=VECTOR ( 'NONE', #8746, 1000.000000000000000 ) ;
#51=CARTESIAN_POINT ( 'NONE',  ( 19.27821517812500574, 117.2309300971526937, 4.728125000614516793 ) ) ;
#52=CARTESIAN_POINT ( 'NONE',  ( 50.59999999999999432, 117.0199925980744666, 4.850000000000000533 ) ) ;
#60=( GEOMETRIC_REPRESENTATION_CONTEXT ( 3 ) GLOBAL_UNCERTAINTY_ASSIGNED_CONTEXT ( ( #12059 ) ) GLOBAL_UNIT_ASSIGNED_CONTEXT ( ( #6222, #10212, #383 ) ) REPRESENTATION_CONTEXT ( 'NONE', 'WORKASPACE' ) );
#64=CARTESIAN_POINT ( 'NONE',  ( 42.76092309580126027, 120.3492821251987550, 2.999999999999998668 ) ) ;
#66=AXIS2_PLACEMENT_3D ( 'NONE', #9653, #8676, #680 ) ;
#73=CARTESIAN_POINT ( 'NONE',  ( 66.44356964374999563, 71.84604660189820891, 4.146875000614517859 ) ) ;
#90=CARTESIAN_POINT ( 'NONE',  ( 3.800000000000001155, 108.0133283987163111, 4.175000001229035362 ) ) ;
#98=CARTESIAN_POINT ( 'NONE',  ( 66.19999999999993179, 71.98667160128364628, 3.837499999999999911 ) ) ;
#114=CARTESIAN_POINT ( 'NONE',  ( 66.44356964374999563, 71.84604660189820891, 4.090625000614517504 ) ) ;
#120=CARTESIAN_POINT ( 'NONE',  ( 19.27821517812503060, 62.76906990284727783, 3.078125000614517326 ) ) ;
#124=CARTESIAN_POINT ( 'NONE',  ( 50.60000000000001563, 62.98000740192552627, 4.250000000000000000 ) ) ;
#129=CARTESIAN_POINT ( 'NONE',  ( 59.24587011312613072, 109.7457631344924778, 2.999999999999999556 ) ) ;
#137=CARTESIAN_POINT ( 'NONE',  ( 66.44356964374998142, 108.1539533981018053, 3.321875000614517237 ) ) ;
#167=CYLINDRICAL_SURFACE ( 'NONE', #2062, 31.19999999999999929 ) ;
#176=CARTESIAN_POINT ( 'NONE',  ( 50.72178482187499071, 117.2309300971526937, 3.753125000614517592 ) ) ;
#183=CARTESIAN_POINT ( 'NONE',  ( 50.72178482187499071, 117.2309300971526937, 4.203125000614517326 ) ) ;
#188=EDGE_CURVE ( 'NONE', #5860, #7119, #2800, .T. ) ;
#201=CARTESIAN_POINT ( 'NONE',  ( 35.00000000000000711, 53.69209320379640360, 4.071875000614516793 ) ) ;
#207=DIRECTION ( 'NONE',  ( -1.000000000000000000, 0.000000000000000000, 0.000000000000000000 ) ) ;
#218=AXIS2_PLACEMENT_3D ( 'NONE', #4134, #11252, #317 ) ;
#234=CARTESIAN_POINT ( 'NONE',  ( 2.300000000000003375, 90.00000000000000000, 3.000000000000000000 ) ) ;
#241=CARTESIAN_POINT ( 'NONE',  ( 50.72178482187501203, 62.76906990284730625, 3.603125000614517681 ) ) ;
#257=ORIENTED_EDGE ( 'NONE', *, *, #8326, .F. ) ;
#276=DIRECTION ( 'NONE',  ( 1.000000000000000000, 0.000000000000000000, 0.000000000000000000 ) ) ;
#277=CARTESIAN_POINT ( 'NONE',  ( 3.556430356250014579, 108.1539533981018053, 3.471875000614516704 ) ) ;
#282=PRODUCT ( 'lid', 'lid', '', ( #4128 ) ) ;
#293=VECTOR ( 'NONE', #10096, 1000.000000000000000 ) ;
#295=( BOUNDED_CURVE ( )  B_SPLINE_CURVE ( 2, ( #8455, #11652, #1581, #11588, #2506, #12579, #9564 ),
 .UNSPECIFIED., .F., .F. ) 
 B_SPLINE_CURVE_WITH_KNOTS ( ( 3, 2, 2, 3 ),
 ( 0.5999999999999999778, 0.6333333333333334147, 0.6666666666666667407, 0.7000000000000001776 ),
 .UNSPECIFIED. ) 
 CURVE ( )  GEOMETRIC_REPRESENTATION_ITEM ( )  RATIONAL_B_SPLINE_CURVE ( ( 1.000000000000000000, 0.8660254037844387076, 1.000000000000000000, 0.8660254037844387076, 1.000000000000000000, 0.8660254037844378194, 1.000000000000000888 ) ) 
 REPRESENTATION_ITEM ( '' )  );
#298=ORIENTED_EDGE ( 'NONE', *, *, #5640, .T. ) ;
#300=EDGE_CURVE ( 'NONE', #9165, #9156, #9132, .T. ) ;
#304=VECTOR ( 'NONE', #4833, 1000.000000000000000 ) ;
#311=CARTESIAN_POINT ( 'NONE',  ( 50.72178482187501203, 62.76906990284730625, 4.053125000614517859 ) ) ;
#317=DIRECTION ( 'NONE',  ( 1.000000000000000000, 0.000000000000000000, 0.000000000000000000 ) ) ;
#332=CARTESIAN_POINT ( 'NONE',  ( 8.335915615093540509, 106.7866562222949938, 3.000000000000001776 ) ) ;
#340=CARTESIAN_POINT ( 'NONE',  ( 66.19999999999998863, 90.00000000000000000, 4.325000000000000178 ) ) ;
#345=CARTESIAN_POINT ( 'NONE',  ( 35.00000000000000711, 53.69209320379639649, 3.621875000614517059 ) ) ;
#373=CARTESIAN_POINT ( 'NONE',  ( 37.09602683542106405, 121.2793079999285339, 2.999999999999998668 ) ) ;
#374=CARTESIAN_POINT ( 'NONE',  ( 66.19999999999997442, 108.0133283987163253, 4.025000001229034119 ) ) ;
#375=ADVANCED_FACE ( 'NONE', ( #11618, #11680 ), #2535, .T. ) ;
#379=AXIS2_PLACEMENT_3D ( 'NONE', #7414, #9573, #11532 ) ;
#383=( NAMED_UNIT ( * ) SI_UNIT ( $, .STERADIAN. ) SOLID_ANGLE_UNIT ( ) );
#391=CARTESIAN_POINT ( 'NONE',  ( 50.72178482187501203, 62.76906990284730625, 4.109375000614517326 ) ) ;
#394=CARTESIAN_POINT ( 'NONE',  ( 33.50000000000000711, 67.79999999999999716, 8.000000000000000000 ) ) ;
#395=CARTESIAN_POINT ( 'NONE',  ( 3.591865698314129496, 91.49237114305354623, 2.999999999999999556 ) ) ;
#415=CARTESIAN_POINT ( 'NONE',  ( 50.60000000000001563, 62.98000740192552627, 4.362500001229034474 ) ) ;
#422=EDGE_CURVE ( 'NONE', #998, #10285, #11419, .T. ) ;
#428=CARTESIAN_POINT ( 'NONE',  ( 66.44356964374999563, 90.00000000000000000, 3.228125000614517237 ) ) ;
#437=CARTESIAN_POINT ( 'NONE',  ( 60.02959220194507139, 108.7322598613235414, 2.999999999999999556 ) ) ;
#439=CARTESIAN_POINT ( 'NONE',  ( 3.800000000000015365, 108.0133283987163111, 3.725000001229034297 ) ) ;
#451=VERTEX_POINT ( 'NONE', #10505 ) ;
#453=EDGE_CURVE ( 'NONE', #9165, #12799, #1651, .T. ) ;
#455=CARTESIAN_POINT ( 'NONE',  ( 64.54728994471078352, 100.7543353520590870, 2.858851390178780871 ) ) ;
#456=ORIENTED_EDGE ( 'NONE', *, *, #7665, .T. ) ;
#480=CARTESIAN_POINT ( 'NONE',  ( 3.800000000000004707, 90.00000000000000000, 6.000000000000000000 ) ) ;
#482=ADVANCED_FACE ( 'NONE', ( #1540, #5532 ), #12604, .F. ) ;
#490=AXIS2_PLACEMENT_3D ( 'NONE', #552, #3647, #7627 ) ;
#494=DIRECTION ( 'NONE',  ( 1.000000000000000000, 0.000000000000000000, 0.000000000000000000 ) ) ;
#525=CARTESIAN_POINT ( 'NONE',  ( 3.556430356250015024, 90.00000000000000000, 3.959375000614517415 ) ) ;
#528=CARTESIAN_POINT ( 'NONE',  ( 3.737990899702874348, 93.52352325000568101, 3.000000000000000000 ) ) ;
#542=CARTESIAN_POINT ( 'NONE',  ( 19.40000000000000924, 117.0199925980744666, 3.687500001229034208 ) ) ;
#552=CARTESIAN_POINT ( 'NONE',  ( 35.00000000000000000, 90.00000000000000000, 6.000000000000000000 ) ) ;
#553=ORIENTED_EDGE ( 'NONE', *, *, #4093, .T. ) ;
#564=CARTESIAN_POINT ( 'NONE',  ( 45.39999948872177526, 60.58435772187547030, 3.000000000000000000 ) ) ;
#582=CARTESIAN_POINT ( 'NONE',  ( 35.39078165856646763, 58.73470357045291479, 3.000000000000001332 ) ) ;
#591=CARTESIAN_POINT ( 'NONE',  ( 3.556430356250015024, 90.00000000000000000, 3.509375000614517681 ) ) ;
#612=CARTESIAN_POINT ( 'NONE',  ( 50.59999999999999432, 117.0199925980744666, 4.400000000000000355 ) ) ;
#618=CARTESIAN_POINT ( 'NONE',  ( 48.11036777325283964, 61.54261756562988239, 3.006515308376277229 ) ) ;
#641=CARTESIAN_POINT ( 'NONE',  ( 19.40000000000002700, 62.98000740192551206, 3.837500001229034563 ) ) ;
#648=CARTESIAN_POINT ( 'NONE',  ( 15.29066239423023887, 65.64213830996915533, 3.000000000000000444 ) ) ;
#656=CARTESIAN_POINT ( 'NONE',  ( 50.72178482187501203, 62.76906990284730625, 3.209375000614517415 ) ) ;
#680=DIRECTION ( 'NONE',  ( 1.000000000000000000, 0.000000000000000000, -0.000000000000000000 ) ) ;
#687=ORIENTED_EDGE ( 'NONE', *, *, #453, .F. ) ;
#696=ORIENTED_EDGE ( 'NONE', *, *, #6826, .F. ) ;
#722=CARTESIAN_POINT ( 'NONE',  ( 3.556430356250014579, 108.1539533981018053, 3.865625000614517415 ) ) ;
#744=CARTESIAN_POINT ( 'NONE',  ( 66.20000000000000284, 71.98667160128370313, 4.287500000000000533 ) ) ;
#748=DIRECTION ( 'NONE',  ( 0.000000000000000000, 0.000000000000000000, -1.000000000000000000 ) ) ;
#754=CARTESIAN_POINT ( 'NONE',  ( 3.556430356250015024, 90.00000000000000000, 4.859375000614517326 ) ) ;
#757=CARTESIAN_POINT ( 'NONE',  ( 3.800000000000001155, 108.0133283987163111, 4.512500000000001066 ) ) ;
#783=CARTESIAN_POINT ( 'NONE',  ( 64.54728994471078352, 100.7543353520590870, 2.802601390178781404 ) ) ;
#795=CARTESIAN_POINT ( 'NONE',  ( 64.24207199149496716, 100.8784753363798075, 2.999999999999999556 ) ) ;
#798=( BOUNDED_CURVE ( )  B_SPLINE_CURVE ( 2, ( #1403, #9385, #542, #2657, #11475, #10628, #6566 ),
 .UNSPECIFIED., .F., .F. ) 
 B_SPLINE_CURVE_WITH_KNOTS ( ( 3, 2, 2, 3 ),
 ( 0.3999999999999999667, 0.4333333333333333481, 0.4666666666666667296, 0.5000000000000001110 ),
 .UNSPECIFIED. ) 
 CURVE ( )  GEOMETRIC_REPRESENTATION_ITEM ( )  RATIONAL_B_SPLINE_CURVE ( ( 1.000000000000000444, 0.8660254037844385966, 1.000000000000000000, 0.8660254037844387076, 1.000000000000000000, 0.8660254037844382635, 1.000000000000000444 ) ) 
 REPRESENTATION_ITEM ( '' )  );
#804=CARTESIAN_POINT ( 'NONE',  ( 50.59999999999999432, 117.0199925980744666, 4.850000000000000533 ) ) ;
#815=CARTESIAN_POINT ( 'NONE',  ( 19.27821517812500574, 117.2309300971526937, 3.884375000614516793 ) ) ;
#831=EDGE_CURVE ( 'NONE', #10785, #11574, #3505, .T. ) ;
#837=ORIENTED_EDGE ( 'NONE', *, *, #6720, .T. ) ;
#856=CARTESIAN_POINT ( 'NONE',  ( 3.800000000000015365, 90.00000000000000000, 4.549999999999999822 ) ) ;
#868=CARTESIAN_POINT ( 'NONE',  ( 50.60000000000001563, 62.98000740192552627, 3.350000000000000533 ) ) ;
#877=CARTESIAN_POINT ( 'NONE',  ( 19.27821517812500574, 117.2309300971526937, 4.334375000614516971 ) ) ;
#906=CARTESIAN_POINT ( 'NONE',  ( 39.63969097257307794, 121.0132401377472036, 3.000000000000001776 ) ) ;
#908=CARTESIAN_POINT ( 'NONE',  ( 19.27821517812503060, 62.76906990284727783, 4.428125000614516971 ) ) ;
#925=CIRCLE ( 'NONE', #9082, 32.70000000000000995 ) ;
#950=DIRECTION ( 'NONE',  ( 0.000000000000000000, 0.000000000000000000, 1.000000000000000000 ) ) ;
#953=DIRECTION ( 'NONE',  ( 1.000000000000000000, 0.000000000000000000, 0.000000000000000000 ) ) ;
#966=CARTESIAN_POINT ( 'NONE',  ( 36.50000000000001421, 67.79999999999999716, 6.000000000000000000 ) ) ;
#974=ORIENTED_EDGE ( 'NONE', *, *, #4443, .F. ) ;
#975=CARTESIAN_POINT ( 'NONE',  ( 66.44356964374999563, 71.84604660189820891, 4.090625000614517504 ) ) ;
#979=CARTESIAN_POINT ( 'NONE',  ( 3.556430356250014579, 108.1539533981018053, 4.765625000614517326 ) ) ;
#998=VERTEX_POINT ( 'NONE', #7937 ) ;
#999=CARTESIAN_POINT ( 'NONE',  ( 60.63303221600038739, 111.5086687461494392, 2.885734441893565538 ) ) ;
#1013=VECTOR ( 'NONE', #9574, 1000.000000000000000 ) ;
#1038=CARTESIAN_POINT ( 'NONE',  ( 66.44356964374999563, 71.84604660189820891, 4.540625000614517681 ) ) ;
#1045=CARTESIAN_POINT ( 'NONE',  ( 3.591865698314129496, 91.49237114305354623, 2.999999999999999556 ) ) ;
#1066=SHAPE_REPRESENTATION ( 'lid', ( #5704 ), #60 ) ;
#1073=CARTESIAN_POINT ( 'NONE',  ( 3.556430356250015024, 90.00000000000000000, 3.509375000614517681 ) ) ;
#1075=CARTESIAN_POINT ( 'NONE',  ( 3.800000000000004707, 90.00000000000000000, 6.000000000000000000 ) ) ;
#1077=EDGE_CURVE ( 'NONE', #11420, #3844, #10237, .T. ) ;
#1102=CARTESIAN_POINT ( 'NONE',  ( 19.27821517812500574, 117.2309300971526937, 2.928125000614517415 ) ) ;
#1109=CARTESIAN_POINT ( 'NONE',  ( 66.44356964375000985, 71.84604660189820891, 4.090625000614517504 ) ) ;
#1127=CARTESIAN_POINT ( 'NONE',  ( 66.44356964374999563, 71.84604660189820891, 3.696875000614517237 ) ) ;
#1139=EDGE_CURVE ( 'NONE', #7089, #12205, #10997, .T. ) ;
#1168=ORIENTED_EDGE ( 'NONE', *, *, #4161, .T. ) ;
#1170=CARTESIAN_POINT ( 'NONE',  ( 66.19999999999998863, 90.00000000000000000, 4.437500001229033764 ) ) ;
#1171=EDGE_CURVE ( 'NONE', #11574, #9287, #1498, .T. ) ;
#1178=CARTESIAN_POINT ( 'NONE',  ( 50.72178482187501203, 62.76906990284730625, 4.053125000614517859 ) ) ;
#1195=ORIENTED_EDGE ( 'NONE', *, *, #453, .T. ) ;
#1238=CARTESIAN_POINT ( 'NONE',  ( 35.00000000000000000, 126.3079067962035822, 3.790625000614517237 ) ) ;
#1242=CARTESIAN_POINT ( 'NONE',  ( 66.19999999999998863, 90.00000000000000000, 3.537500001229034297 ) ) ;
#1246=CARTESIAN_POINT ( 'NONE',  ( 3.556430356250014579, 108.1539533981018053, 3.415625000614516793 ) ) ;
#1277=DIRECTION ( 'NONE',  ( -0.000000000000000000, -0.000000000000000000, -1.000000000000000000 ) ) ;
#1297=EDGE_LOOP ( 'NONE', ( #7827, #837, #9546, #8819, #11893, #3996 ) ) ;
#1302=CARTESIAN_POINT ( 'NONE',  ( 3.556430356250015024, 90.00000000000000000, 3.453125000614517770 ) ) ;
#1310=( NAMED_UNIT ( * ) PLANE_ANGLE_UNIT ( ) SI_UNIT ( $, .RADIAN. ) );
#1317=ORIENTED_EDGE ( 'NONE', *, *, #10037, .F. ) ;
#1321=CARTESIAN_POINT ( 'NONE',  ( 6.262912888864590855, 102.7722879626690400, 3.000000000000000888 ) ) ;
#1333=LINE ( 'NONE', #9323, #4401 ) ;
#1385=FACE_OUTER_BOUND ( 'NONE', #5050, .T. ) ;
#1394=DIRECTION ( 'NONE',  ( -0.000000000000000000, -0.000000000000000000, -1.000000000000000000 ) ) ;
#1403=CARTESIAN_POINT ( 'NONE',  ( 3.800000000000015365, 90.00000000000000000, 3.762500001229034385 ) ) ;
#1409=EDGE_CURVE ( 'NONE', #3535, #10249, #5810, .T. ) ;
#1430=CARTESIAN_POINT ( 'NONE',  ( 57.53855666881469233, 111.6893844235947881, 2.999999999999999112 ) ) ;
#1432=CARTESIAN_POINT ( 'NONE',  ( 3.800000000000015365, 90.00000000000000000, 2.862500001229034474 ) ) ;
#1442=SURFACE_STYLE_USAGE ( .BOTH. , #10276 ) ;
#1445=VECTOR ( 'NONE', #1786, 1000.000000000000000 ) ;
#1446=ORIENTED_EDGE ( 'NONE', *, *, #3128, .T. ) ;
#1476=CARTESIAN_POINT ( 'NONE',  ( 66.19999999999988916, 71.98667160128361786, 4.737499999999998934 ) ) ;
#1498=LINE ( 'NONE', #8974, #7202 ) ;
#1506=CARTESIAN_POINT ( 'NONE',  ( 21.76320231625934554, 61.63142451696531765, 3.000000000000000000 ) ) ;
#1515=CARTESIAN_POINT ( 'NONE',  ( 3.556430356250028790, 71.84604660189818048, 4.446875000614517681 ) ) ;
#1519=CARTESIAN_POINT ( 'NONE',  ( 4.418411362812244114, 97.51822454362397252, 3.000000000000000444 ) ) ;
#1526=CARTESIAN_POINT ( 'NONE',  ( 66.19999999999998863, 90.00000000000000000, 3.087500001229034119 ) ) ;
#1529=DIRECTION ( 'NONE',  ( 0.000000000000000000, 0.000000000000000000, 1.000000000000000000 ) ) ;
#1540=FACE_BOUND ( 'NONE', #3300, .T. ) ;
#1542=ORIENTED_EDGE ( 'NONE', *, *, #10710, .F. ) ;
#1566=CARTESIAN_POINT ( 'NONE',  ( 66.20000000000000284, 71.98667160128370313, 3.950000001229034829 ) ) ;
#1568=DIRECTION ( 'NONE',  ( -0.000000000000000000, -0.000000000000000000, -1.000000000000000000 ) ) ;
#1581=CARTESIAN_POINT ( 'NONE',  ( 19.40000000000000924, 117.0199925980744666, 3.237500001229034030 ) ) ;
#1584=CARTESIAN_POINT ( 'NONE',  ( 3.556430356250014579, 108.1539533981018053, 4.371875000614517504 ) ) ;
#1592=FACE_OUTER_BOUND ( 'NONE', #9632, .T. ) ;
#1601=CARTESIAN_POINT ( 'NONE',  ( 36.50000000000001421, 79.80000000000001137, 6.000000000000000000 ) ) ;
#1606=CARTESIAN_POINT ( 'NONE',  ( 19.40000000000000924, 117.0199925980744666, 4.474999999999999645 ) ) ;
#1614=CARTESIAN_POINT ( 'NONE',  ( 3.800000000000015365, 90.00000000000000000, 4.212500001229034119 ) ) ;
#1633=CARTESIAN_POINT ( 'NONE',  ( 3.800000000000025135, 71.98667160128366049, 3.800000001229034030 ) ) ;
#1640=CARTESIAN_POINT ( 'NONE',  ( 3.535514453314946071, 90.20686785236708261, 2.999999999999999556 ) ) ;
#1644=ORIENTED_EDGE ( 'NONE', *, *, #12182, .T. ) ;
#1649=CARTESIAN_POINT ( 'NONE',  ( 3.556430356250015024, 90.00000000000000000, 4.859375000614517326 ) ) ;
#1651=( BOUNDED_CURVE ( )  B_SPLINE_CURVE ( 2, ( #8419, #4558, #5599, #618, #6704 ),
 .UNSPECIFIED., .F., .F. ) 
 B_SPLINE_CURVE_WITH_KNOTS ( ( 3, 2, 3 ),
 ( 0.7000000000000001776, 0.7333333333333332815, 0.7393280224290094127 ),
 .UNSPECIFIED. ) 
 CURVE ( )  GEOMETRIC_REPRESENTATION_ITEM ( )  RATIONAL_B_SPLINE_CURVE ( ( 0.9999999999999991118, 0.8660254037844395958, 1.000000000000000000, 0.9759059184690689337, 0.9604780286075660367 ) ) 
 REPRESENTATION_ITEM ( '' )  );
#1666=PLANE ( 'NONE',  #8597 ) ;
#1670=CARTESIAN_POINT ( 'NONE',  ( 35.00000000000000000, 126.0266567974326222, 4.437500000000000888 ) ) ;
#1705=CARTESIAN_POINT ( 'NONE',  ( 36.66058250612193348, 58.78194026151831508, 3.000000000000000000 ) ) ;
#1714=CARTESIAN_POINT ( 'NONE',  ( 66.44356964374999563, 71.84604660189820891, 3.190625000614517592 ) ) ;
#1723=CYLINDRICAL_SURFACE ( 'NONE', #4906, 31.19999999999999929 ) ;
#1728=CARTESIAN_POINT ( 'NONE',  ( 3.800000000000015365, 90.00000000000000000, 4.831250000614517148 ) ) ;
#1730=CARTESIAN_POINT ( 'NONE',  ( 33.50000000000000711, 79.80000000000001137, 8.000000000000000000 ) ) ;
#1733=CARTESIAN_POINT ( 'NONE',  ( 50.59999999999999432, 117.0199925980744666, 3.050000000000000266 ) ) ;
#1737=DIRECTION ( 'NONE',  ( -0.000000000000000000, -0.000000000000000000, -1.000000000000000000 ) ) ;
#1743=CARTESIAN_POINT ( 'NONE',  ( 35.00000000000000000, 126.3079067962036106, 4.296875000614517326 ) ) ;
#1761=ORIENTED_EDGE ( 'NONE', *, *, #2695, .T. ) ;
#1764=ORIENTED_EDGE ( 'NONE', *, *, #2695, .F. ) ;
#1770=VECTOR ( 'NONE', #1737, 1000.000000000000000 ) ;
#1779=VERTEX_POINT ( 'NONE', #1614 ) ;
#1786=DIRECTION ( 'NONE',  ( -0.000000000000000000, -1.000000000000000000, -0.000000000000000000 ) ) ;
#1798=CARTESIAN_POINT ( 'NONE',  ( 66.19999999999997442, 108.0133283987163253, 4.812500000000000000 ) ) ;
#1801=EDGE_LOOP ( 'NONE', ( #4383, #257 ) ) ;
#1804=CYLINDRICAL_SURFACE ( 'NONE', #11999, 32.70000000000000284 ) ;
#1824=VECTOR ( 'NONE', #494, 1000.000000000000000 ) ;
#1842=ORIENTED_EDGE ( 'NONE', *, *, #9583, .T. ) ;
#1843=CARTESIAN_POINT ( 'NONE',  ( 50.72178482187499071, 117.2309300971526937, 3.753125000614517592 ) ) ;
#1851=CARTESIAN_POINT ( 'NONE',  ( 33.50000000000000711, 67.79999999999999716, 8.000000000000000000 ) ) ;
#1859=LINE ( 'NONE', #5846, #2536 ) ;
#1864=CARTESIAN_POINT ( 'NONE',  ( 3.800000000000015365, 90.00000000000000000, 3.650000000000000355 ) ) ;
#1867=AXIS2_PLACEMENT_3D ( 'NONE', #7290, #11337, #207 ) ;
#1874=CARTESIAN_POINT ( 'NONE',  ( 66.44356964374999563, 90.00000000000000000, 4.634375000614516793 ) ) ;
#1897=CARTESIAN_POINT ( 'NONE',  ( 66.19999999999998863, 90.00000000000000000, 3.425000000000000266 ) ) ;
#1905=CARTESIAN_POINT ( 'NONE',  ( 35.00000000000000711, 53.69209320379640360, 4.015625000614517326 ) ) ;
#1918=CARTESIAN_POINT ( 'NONE',  ( 14.50114310663104966, 113.8451850114809361, 2.999999999999999112 ) ) ;
#1925=EDGE_LOOP ( 'NONE', ( #8389, #9356, #4884, #1317 ) ) ;
#1926=CARTESIAN_POINT ( 'NONE',  ( 50.72178482187499071, 117.2309300971526937, 2.909375000614517148 ) ) ;
#1927=CARTESIAN_POINT ( 'NONE',  ( 66.19999999999998863, 90.00000000000000000, 4.774999999999999467 ) ) ;
#1935=CARTESIAN_POINT ( 'NONE',  ( 66.44356964374998142, 108.1539533981018053, 4.671875000614517326 ) ) ;
#1940=LINE ( 'NONE', #9981, #49 ) ;
#1971=CARTESIAN_POINT ( 'NONE',  ( 35.00000000000000000, 126.3079067962035822, 3.790625000614517237 ) ) ;
#1975=CARTESIAN_POINT ( 'NONE',  ( 19.27821517812500574, 117.2309300971526937, 3.378125000614517148 ) ) ;
#1993=CARTESIAN_POINT ( 'NONE',  ( 66.44356964374999563, 90.00000000000000000, 3.284375000614517148 ) ) ;
#2006=CARTESIAN_POINT ( 'NONE',  ( 3.556430356250028790, 71.84604660189818048, 4.446875000614517681 ) ) ;
#2031=DIRECTION ( 'NONE',  ( -0.000000000000000000, -0.000000000000000000, -1.000000000000000000 ) ) ;
#2033=CARTESIAN_POINT ( 'NONE',  ( 66.19999999999997442, 108.0133283987163253, 4.475000001229034297 ) ) ;
#2039=CARTESIAN_POINT ( 'NONE',  ( 50.72178482187499071, 117.2309300971526937, 4.653125000614517504 ) ) ;
#2049=CARTESIAN_POINT ( 'NONE',  ( 51.56500827743923310, 116.5679260320323323, 3.000000000000000000 ) ) ;
#2057=ORIENTED_EDGE ( 'NONE', *, *, #422, .T. ) ;
#2062=AXIS2_PLACEMENT_3D ( 'NONE', #4186, #8173, #7186 ) ;
#2083=CARTESIAN_POINT ( 'NONE',  ( 19.40000000000002700, 62.98000740192551206, 3.725000000000000089 ) ) ;
#2100=CARTESIAN_POINT ( 'NONE',  ( 3.556430356250028790, 71.84604660189818048, 4.390625000614517326 ) ) ;
#2107=CARTESIAN_POINT ( 'NONE',  ( 3.556430356250028790, 71.84604660189818048, 3.040625000614517681 ) ) ;
#2116=CARTESIAN_POINT ( 'NONE',  ( 50.47081135474928715, 117.2246076195576734, 3.000000000000001332 ) ) ;
#2124=CARTESIAN_POINT ( 'NONE',  ( 19.27821517812500574, 117.2309300971526937, 3.884375000614516793 ) ) ;
#2141=CARTESIAN_POINT ( 'NONE',  ( 66.19999999999998863, 90.00000000000000000, 3.987500001229034030 ) ) ;
#2146=CARTESIAN_POINT ( 'NONE',  ( 3.800000000000004707, 90.00000000000000000, 6.000000000000000000 ) ) ;
#2162=CARTESIAN_POINT ( 'NONE',  ( 19.27821517812503060, 62.76906990284727783, 3.078125000614517326 ) ) ;
#2164=CARTESIAN_POINT ( 'NONE',  ( 3.800000000000015365, 90.00000000000000000, 3.312500001229034652 ) ) ;
#2172=CARTESIAN_POINT ( 'NONE',  ( 66.44356964374999563, 90.00000000000000000, 4.578125000614516438 ) ) ;
#2178=PRODUCT_DEFINITION_FORMATION_WITH_SPECIFIED_SOURCE ( 'ANY', '', #282, .NOT_KNOWN. ) ;
#2186=ORIENTED_EDGE ( 'NONE', *, *, #7665, .F. ) ;
#2191=CARTESIAN_POINT ( 'NONE',  ( 50.72178482187501203, 62.76906990284730625, 4.109375000614517326 ) ) ;
#2204=CARTESIAN_POINT ( 'NONE',  ( 19.27821517812503060, 62.76906990284727783, 3.134375000614517237 ) ) ;
#2206=AXIS2_PLACEMENT_3D ( 'NONE', #5682, #7902, #11889 ) ;
#2211=CARTESIAN_POINT ( 'NONE',  ( 50.59999999999999432, 117.0199925980744666, 4.062500001229034652 ) ) ;
#2226=ORIENTED_EDGE ( 'NONE', *, *, #3194, .F. ) ;
#2232=CARTESIAN_POINT ( 'NONE',  ( 33.50000000000000711, 67.79999999999999716, 8.000000000000000000 ) ) ;
#2233=ORIENTED_EDGE ( 'NONE', *, *, #8141, .T. ) ;
#2235=CARTESIAN_POINT ( 'NONE',  ( 19.27821517812503060, 62.76906990284727783, 3.978125000614516793 ) ) ;
#2243=CARTESIAN_POINT ( 'NONE',  ( 66.44356964375000985, 71.84604660189820891, 3.640625000614517326 ) ) ;
#2271=CARTESIAN_POINT ( 'NONE',  ( 13.53859087060910404, 112.9805567844265397, 2.999999999999999112 ) ) ;
#2277=DIRECTION ( 'NONE',  ( -1.000000000000000000, 0.000000000000000000, 0.000000000000000000 ) ) ;
#2283=EDGE_CURVE ( 'NONE', #11574, #998, #4613, .T. ) ;
#2284=PLANE ( 'NONE',  #12748 ) ;
#2287=DIRECTION ( 'NONE',  ( -0.000000000000000000, -0.000000000000000000, -1.000000000000000000 ) ) ;
#2301=CARTESIAN_POINT ( 'NONE',  ( 19.27821517812500574, 117.2309300971526937, 4.728125000614516793 ) ) ;
#2333=CARTESIAN_POINT ( 'NONE',  ( 35.00000000000000711, 53.69209320379639649, 3.171875000614517326 ) ) ;
#2342=ORIENTED_EDGE ( 'NONE', *, *, #3931, .F. ) ;
#2360=CARTESIAN_POINT ( 'NONE',  ( 19.40000000000002700, 62.98000740192551206, 2.937500001229034208 ) ) ;
#2379=PLANE ( 'NONE',  #5446 ) ;
#2386=LINE ( 'NONE', #12588, #12100 ) ;
#2427=CARTESIAN_POINT ( 'NONE',  ( 3.800000000000015365, 90.00000000000000000, 4.212500001229034119 ) ) ;
#2438=FILL_AREA_STYLE_COLOUR ( '', #6750 ) ;
#2444=CARTESIAN_POINT ( 'NONE',  ( 66.44356964374999563, 90.00000000000000000, 3.734375000614516882 ) ) ;
#2492=CARTESIAN_POINT ( 'NONE',  ( 35.00000000000000711, 53.97334320256736362, 2.975000001229034741 ) ) ;
#2499=CARTESIAN_POINT ( 'NONE',  ( 20.61329739217925194, 62.19155013526994935, 3.000000000000000444 ) ) ;
#2503=ORIENTED_EDGE ( 'NONE', *, *, #9032, .T. ) ;
#2506=CARTESIAN_POINT ( 'NONE',  ( 50.59999999999999432, 117.0199925980744666, 3.162500001229034741 ) ) ;
#2508=CARTESIAN_POINT ( 'NONE',  ( 35.00000000000000000, 126.3079067962035822, 4.296875000614517326 ) ) ;
#2517=LINE ( 'NONE', #8403, #1013 ) ;
#2535=PLANE ( 'NONE',  #66 ) ;
#2536=VECTOR ( 'NONE', #10878, 1000.000000000000000 ) ;
#2554=CARTESIAN_POINT ( 'NONE',  ( 35.00000000000000711, 53.97334320256736362, 3.425000001229034474 ) ) ;
#2557=FACE_OUTER_BOUND ( 'NONE', #5571, .T. ) ;
#2561=CARTESIAN_POINT ( 'NONE',  ( 40.44561422048254684, 59.23121341156224418, 2.999999999999998668 ) ) ;
#2571=CARTESIAN_POINT ( 'NONE',  ( 19.27821517812503060, 62.76906990284727783, 3.134375000614517237 ) ) ;
#2590=CARTESIAN_POINT ( 'NONE',  ( 3.800000000000025135, 71.98667160128366049, 3.237500000000000266 ) ) ;
#2606=ORIENTED_EDGE ( 'NONE', *, *, #3931, .T. ) ;
#2620=CARTESIAN_POINT ( 'NONE',  ( 50.60000000000001563, 62.98000740192552627, 3.912500001229034297 ) ) ;
#2629=CARTESIAN_POINT ( 'NONE',  ( 4.785832313128271842, 81.33916431800814451, 2.999999999999999112 ) ) ;
#2638=ORIENTED_EDGE ( 'NONE', *, *, #4093, .F. ) ;
#2640=CARTESIAN_POINT ( 'NONE',  ( 19.27821517812500574, 117.2309300971526937, 3.434375000614517059 ) ) ;
#2641=ORIENTED_EDGE ( 'NONE', *, *, #9032, .F. ) ;
#2647=ADVANCED_FACE ( 'NONE', ( #1385 ), #11076, .T. ) ;
#2657=CARTESIAN_POINT ( 'NONE',  ( 35.00000000000000000, 126.0266567974326222, 3.650000001229033675 ) ) ;
#2659=CARTESIAN_POINT ( 'NONE',  ( 19.40000000000000924, 117.0199925980744666, 4.025000000000000355 ) ) ;
#2673=CARTESIAN_POINT ( 'NONE',  ( 50.59999999999999432, 117.0199925980744666, 4.400000000000000355 ) ) ;
#2688=EDGE_LOOP ( 'NONE', ( #10332, #2797, #7879, #9218, #1446, #2784, #5155, #2606, #1761, #1842, #1195 ) ) ;
#2689=CARTESIAN_POINT ( 'NONE',  ( 33.50000000000000711, 67.79999999999999716, 8.000000000000000000 ) ) ;
#2691=AXIS2_PLACEMENT_3D ( 'NONE', #3323, #6315, #2277 ) ;
#2695=EDGE_CURVE ( 'NONE', #12353, #5750, #10666, .T. ) ;
#2704=CARTESIAN_POINT ( 'NONE',  ( 3.556430356250028790, 71.84604660189818048, 3.490625000614517415 ) ) ;
#2723=CARTESIAN_POINT ( 'NONE',  ( 3.800000000000015365, 108.0133283987163111, 3.162500000000000533 ) ) ;
#2757=CARTESIAN_POINT ( 'NONE',  ( 9.934812860078272578, 71.14691728539177973, 3.000000000000000444 ) ) ;
#2767=CARTESIAN_POINT ( 'NONE',  ( 35.00000000000000000, 126.3079067962035822, 4.690625000614518036 ) ) ;
#2776=CARTESIAN_POINT ( 'NONE',  ( 64.31840955652157277, 100.6710290542226574, 3.000000000000000000 ) ) ;
#2784=ORIENTED_EDGE ( 'NONE', *, *, #2957, .T. ) ;
#2785=CARTESIAN_POINT ( 'NONE',  ( 35.00000000000000000, 126.0266567974326222, 4.887500000000001066 ) ) ;
#2790=CARTESIAN_POINT ( 'NONE',  ( 35.00000000000000000, 90.00000000000000000, 6.000000000000000000 ) ) ;
#2795=CARTESIAN_POINT ( 'NONE',  ( 3.556430356250015024, 90.00000000000000000, 4.859375000614517326 ) ) ;
#2797=ORIENTED_EDGE ( 'NONE', *, *, #4345, .F. ) ;
#2800=CIRCLE ( 'NONE', #8025, 32.70000000000000995 ) ;
#2829=VECTOR ( 'NONE', #9037, 1000.000000000000000 ) ;
#2850=DIRECTION ( 'NONE',  ( 0.000000000000000000, 0.000000000000000000, 1.000000000000000000 ) ) ;
#2853=CARTESIAN_POINT ( 'NONE',  ( 50.60000000000001563, 62.98000740192552627, 3.800000000000000266 ) ) ;
#2873=CARTESIAN_POINT ( 'NONE',  ( 35.00000000000000000, 90.00000000000000000, 8.000000000000000000 ) ) ;
#2893=CARTESIAN_POINT ( 'NONE',  ( 66.44356964374999563, 90.00000000000000000, 3.228125000614517237 ) ) ;
#2912=CARTESIAN_POINT ( 'NONE',  ( 36.50000000000001421, 67.79999999999999716, 8.000000000000000000 ) ) ;
#2914=CARTESIAN_POINT ( 'NONE',  ( 66.44356964374999563, 71.84604660189820891, 4.596875000614517148 ) ) ;
#2924=CARTESIAN_POINT ( 'NONE',  ( 50.72178482187501203, 62.76906990284730625, 4.109375000614517326 ) ) ;
#2955=CARTESIAN_POINT ( 'NONE',  ( 66.44356964374999563, 90.00000000000000000, 4.578125000614516438 ) ) ;
#2957=EDGE_CURVE ( 'NONE', #1779, #7089, #3911, .T. ) ;
#2958=CARTESIAN_POINT ( 'NONE',  ( 3.800000000000015365, 90.00000000000000000, 4.662500001229034297 ) ) ;
#2959=CARTESIAN_POINT ( 'NONE',  ( 66.44356964374998142, 108.1539533981018053, 3.715625000614517948 ) ) ;
#2967=CARTESIAN_POINT ( 'NONE',  ( 64.26751784650379307, 100.8093265756609185, 3.000000000000000000 ) ) ;
#2976=CARTESIAN_POINT ( 'NONE',  ( 19.27821517812503060, 62.76906990284727783, 4.484375000614516438 ) ) ;
#2987=( BOUNDED_CURVE ( )  B_SPLINE_CURVE ( 2, ( #7499, #4428, #415, #10743, #8784, #7367, #3453 ),
 .UNSPECIFIED., .F., .F. ) 
 B_SPLINE_CURVE_WITH_KNOTS ( ( 3, 2, 2, 3 ),
 ( 0.1000000000000001860, 0.1333333333333334425, 0.1666666666666666852, 0.2000000000000000111 ),
 .UNSPECIFIED. ) 
 CURVE ( )  GEOMETRIC_REPRESENTATION_ITEM ( )  RATIONAL_B_SPLINE_CURVE ( ( 0.9999999999999992228, 0.8660254037844394848, 1.000000000000000000, 0.8660254037844387076, 1.000000000000000000, 0.8660254037844388186, 0.9999999999999998890 ) ) 
 REPRESENTATION_ITEM ( '' )  );
#3004=DIRECTION ( 'NONE',  ( -0.000000000000000000, -0.000000000000000000, -1.000000000000000000 ) ) ;
#3012=LINE ( 'NONE', #4255, #9921 ) ;
#3020=CARTESIAN_POINT ( 'NONE',  ( 3.556430356250014135, 90.74660626562589982, 3.001582761613071693 ) ) ;
#3031=CARTESIAN_POINT ( 'NONE',  ( 53.14830700235364702, 115.4796592025445392, 2.999999999999999556 ) ) ;
#3042=CARTESIAN_POINT ( 'NONE',  ( 50.72178482187499071, 117.2309300971526937, 4.709375000614516971 ) ) ;
#3059=EDGE_CURVE ( 'NONE', #8545, #12789, #3193, .T. ) ;
#3066=CARTESIAN_POINT ( 'NONE',  ( 50.60000000000001563, 62.98000740192552627, 3.800000000000000266 ) ) ;
#3072=AXIS2_PLACEMENT_3D ( 'NONE', #2912, #8791, #2850 ) ;
#3083=ORIENTED_EDGE ( 'NONE', *, *, #4687, .F. ) ;
#3085=CARTESIAN_POINT ( 'NONE',  ( 66.44356964374999563, 71.84604660189820891, 3.190625000614517592 ) ) ;
#3090=CARTESIAN_POINT ( 'NONE',  ( 3.556430356250028790, 71.84604660189818048, 3.490625000614516971 ) ) ;
#3109=CARTESIAN_POINT ( 'NONE',  ( 3.556430356250015024, 90.00000000000000000, 4.409375000614517148 ) ) ;
#3114=LINE ( 'NONE', #4223, #293 ) ;
#3118=LINE ( 'NONE', #10171, #7110 ) ;
#3119=CARTESIAN_POINT ( 'NONE',  ( 19.27821517812503060, 62.76906990284727783, 3.584375000614516971 ) ) ;
#3121=LINE ( 'NONE', #1075, #7040 ) ;
#3128=EDGE_CURVE ( 'NONE', #7460, #1779, #2987, .T. ) ;
#3133=FACE_OUTER_BOUND ( 'NONE', #1801, .T. ) ;
#3149=CARTESIAN_POINT ( 'NONE',  ( 3.800000000000015365, 90.00000000000000000, 4.662500001229034297 ) ) ;
#3151=CARTESIAN_POINT ( 'NONE',  ( 19.40000000000002700, 62.98000740192551206, 3.387500001229033941 ) ) ;
#3157=CARTESIAN_POINT ( 'NONE',  ( 19.27821517812503060, 62.76906990284727783, 3.978125000614516793 ) ) ;
#3158=CARTESIAN_POINT ( 'NONE',  ( 19.40000000000000924, 117.0199925980744666, 4.924999999999999822 ) ) ;
#3175=CARTESIAN_POINT ( 'NONE',  ( 35.00000000000000000, 126.3079067962035822, 2.946875000614516793 ) ) ;
#3193=LINE ( 'NONE', #5074, #6588 ) ;
#3194=EDGE_CURVE ( 'NONE', #4984, #9287, #12424, .T. ) ;
#3216=CARTESIAN_POINT ( 'NONE',  ( 50.60000000000001563, 62.98000740192552627, 4.362500001229034474 ) ) ;
#3221=CARTESIAN_POINT ( 'NONE',  ( 35.00000000000000000, 90.00000000000000000, 6.000000000000000000 ) ) ;
#3222=CARTESIAN_POINT ( 'NONE',  ( 3.556430356250014579, 108.1539533981018053, 4.315625000614517148 ) ) ;
#3227=CARTESIAN_POINT ( 'NONE',  ( 19.40000000000002700, 62.98000740192551206, 4.174999999999999822 ) ) ;
#3258=ADVANCED_FACE ( 'NONE', ( #2557 ), #3672, .F. ) ;
#3284=CARTESIAN_POINT ( 'NONE',  ( 66.44356964374999563, 71.84604660189820891, 3.640625000614517326 ) ) ;
#3299=CARTESIAN_POINT ( 'NONE',  ( 60.32621597448488870, 111.4045591870091840, 3.026619673138257749 ) ) ;
#3300=EDGE_LOOP ( 'NONE', ( #6905, #12091, #10348, #6277 ) ) ;
#3317=CARTESIAN_POINT ( 'NONE',  ( 66.44356964374999563, 90.00000000000000000, 3.734375000614516882 ) ) ;
#3319=VECTOR ( 'NONE', #5863, 1000.000000000000000 ) ;
#3323=CARTESIAN_POINT ( 'NONE',  ( 35.00000000000000000, 90.00000000000000000, 6.000000000000000000 ) ) ;
#3343=( BOUNDED_CURVE ( )  B_SPLINE_CURVE ( 2, ( #8606, #11608, #4547, #11669, #3827, #11803, #5589 ),
 .UNSPECIFIED., .F., .F. ) 
 B_SPLINE_CURVE_WITH_KNOTS ( ( 3, 2, 2, 3 ),
 ( 0.5999999999999999778, 0.6333333333333334147, 0.6666666666666667407, 0.7000000000000001776 ),
 .UNSPECIFIED. ) 
 CURVE ( )  GEOMETRIC_REPRESENTATION_ITEM ( )  RATIONAL_B_SPLINE_CURVE ( ( 1.000000000000000000, 0.8660254037844387076, 1.000000000000000000, 0.8660254037844387076, 1.000000000000000000, 0.8660254037844378194, 1.000000000000000888 ) ) 
 REPRESENTATION_ITEM ( '' )  );
#3349=CARTESIAN_POINT ( 'NONE',  ( 3.556430356250015024, 90.00000000000000000, 3.003125000614517148 ) ) ;
#3354=CARTESIAN_POINT ( 'NONE',  ( 3.800000000000015365, 90.00000000000000000, 4.100000000000000533 ) ) ;
#3386=MANIFOLD_SOLID_BREP ( 'Cavity1', #7803 ) ;
#3407=ORIENTED_EDGE ( 'NONE', *, *, #5709, .F. ) ;
#3408=CARTESIAN_POINT ( 'NONE',  ( 35.16468375597256824, 121.3570802786415328, 3.000000000000001332 ) ) ;
#3410=CARTESIAN_POINT ( 'NONE',  ( 66.19999999999997442, 108.0133283987163253, 3.575000001229033941 ) ) ;
#3414=DIRECTION ( 'NONE',  ( -1.000000000000000000, 0.000000000000000000, 0.000000000000000000 ) ) ;
#3424=CARTESIAN_POINT ( 'NONE',  ( 50.72178482187501203, 62.76906990284730625, 4.559375000614517504 ) ) ;
#3453=CARTESIAN_POINT ( 'NONE',  ( 3.800000000000015365, 90.00000000000000000, 4.212500001229034119 ) ) ;
#3466=EDGE_LOOP ( 'NONE', ( #12289, #7761, #5875, #696 ) ) ;
#3475=CARTESIAN_POINT ( 'NONE',  ( 19.40000000000000924, 117.0199925980744666, 4.587500001229034119 ) ) ;
#3492=CARTESIAN_POINT ( 'NONE',  ( 3.556430356250028790, 71.84604660189818048, 3.546875000614516882 ) ) ;
#3495=FACE_OUTER_BOUND ( 'NONE', #10612, .T. ) ;
#3505=LINE ( 'NONE', #7614, #7612 ) ;
#3527=CARTESIAN_POINT ( 'NONE',  ( 64.31840955652157277, 100.6710290542226574, 3.000000000000000000 ) ) ;
#3531=ORIENTED_EDGE ( 'NONE', *, *, #4345, .T. ) ;
#3534=ADVANCED_FACE ( 'NONE', ( #12154 ), #11233, .F. ) ;
#3535=VERTEX_POINT ( 'NONE', #12088 ) ;
#3539=CARTESIAN_POINT ( 'NONE',  ( 50.59999999999999432, 117.0199925980744666, 4.512500001229033941 ) ) ;
#3544=CARTESIAN_POINT ( 'NONE',  ( 36.50000000000001421, 67.79999999999999716, 8.000000000000000000 ) ) ;
#3557=CARTESIAN_POINT ( 'NONE',  ( 50.72178482187499071, 117.2309300971526937, 3.809375000614517504 ) ) ;
#3564=CARTESIAN_POINT ( 'NONE',  ( 66.20000000000000284, 90.00000000000000000, 6.000000000000000000 ) ) ;
#3588=EDGE_LOOP ( 'NONE', ( #1764, #5107, #298, #3083 ) ) ;
#3604=CARTESIAN_POINT ( 'NONE',  ( 66.19999999999998863, 90.00000000000000000, 3.987500001229034030 ) ) ;
#3612=CARTESIAN_POINT ( 'NONE',  ( 25.31483199390188332, 60.14306353880185441, 3.000000000000001332 ) ) ;
#3622=CARTESIAN_POINT ( 'NONE',  ( 35.00000000000000711, 53.69209320379640360, 3.621875000614517059 ) ) ;
#3641=CARTESIAN_POINT ( 'NONE',  ( 50.60000000000001563, 62.98000740192552627, 4.250000000000000000 ) ) ;
#3647=DIRECTION ( 'NONE',  ( 0.000000000000000000, 0.000000000000000000, 1.000000000000000000 ) ) ;
#3672=CYLINDRICAL_SURFACE ( 'NONE', #5338, 31.19999999999999929 ) ;
#3679=CARTESIAN_POINT ( 'NONE',  ( 45.39999948872177526, 60.58435772187547030, 3.000000000000000000 ) ) ;
#3680=CARTESIAN_POINT ( 'NONE',  ( 66.19999999999988916, 71.98667160128361786, 3.387499999999999734 ) ) ;
#3689=CARTESIAN_POINT ( 'NONE',  ( 19.27821517812503060, 62.76906990284727783, 4.034375000614517148 ) ) ;
#3702=CIRCLE ( 'NONE', #10992, 32.70000000000000995 ) ;
#3706=CARTESIAN_POINT ( 'NONE',  ( 66.20000000000000284, 71.98667160128370313, 4.737500000000000711 ) ) ;
#3720=CARTESIAN_POINT ( 'NONE',  ( 35.00000000000000711, 53.97334320256736362, 3.875000001229034208 ) ) ;
#3748=CARTESIAN_POINT ( 'NONE',  ( 35.00000000000000000, 126.3079067962035822, 2.890625000614516882 ) ) ;
#3759=CARTESIAN_POINT ( 'NONE',  ( 3.800000000000015365, 90.00000000000000000, 4.549999999999999822 ) ) ;
#3768=CARTESIAN_POINT ( 'NONE',  ( 3.800000000000015365, 108.0133283987163111, 4.512500000000000178 ) ) ;
#3785=EDGE_CURVE ( 'NONE', #10285, #11420, #11501, .T. ) ;
#3796=( NAMED_UNIT ( * ) PLANE_ANGLE_UNIT ( ) SI_UNIT ( $, .RADIAN. ) );
#3802=CARTESIAN_POINT ( 'NONE',  ( 17.32445633083897008, 64.11686499059005939, 3.000000000000001776 ) ) ;
#3810=CARTESIAN_POINT ( 'NONE',  ( 3.556430356250014579, 108.1539533981018053, 3.415625000614517237 ) ) ;
#3827=CARTESIAN_POINT ( 'NONE',  ( 50.59999999999999432, 117.0199925980744666, 3.500000000000000444 ) ) ;
#3831=CARTESIAN_POINT ( 'NONE',  ( 66.19999999999997442, 108.0133283987163253, 3.912500000000000533 ) ) ;
#3844=VERTEX_POINT ( 'NONE', #9324 ) ;
#3845=VECTOR ( 'NONE', #10634, 1000.000000000000227 ) ;
#3867=CARTESIAN_POINT ( 'NONE',  ( 3.799999999999904787, 71.98667160128373155, 3.237499999999999822 ) ) ;
#3877=CARTESIAN_POINT ( 'NONE',  ( 19.27821517812500574, 117.2309300971526937, 3.828125000614516882 ) ) ;
#3900=CARTESIAN_POINT ( 'NONE',  ( 66.19999999999998863, 90.00000000000000000, 4.774999999999999467 ) ) ;
#3909=CARTESIAN_POINT ( 'NONE',  ( 50.72178482187499071, 117.2309300971526937, 3.809375000614517504 ) ) ;
#3911=( BOUNDED_CURVE ( )  B_SPLINE_CURVE ( 2, ( #11089, #90, #6253, #9198, #2211, #6188, #2141 ),
 .UNSPECIFIED., .F., .F. ) 
 B_SPLINE_CURVE_WITH_KNOTS ( ( 3, 2, 2, 3 ),
 ( 0.1999999999999999833, 0.2333333333333333925, 0.2666666666666668295, 0.3000000000000002109 ),
 .UNSPECIFIED. ) 
 CURVE ( )  GEOMETRIC_REPRESENTATION_ITEM ( )  RATIONAL_B_SPLINE_CURVE ( ( 1.000000000000000222, 0.8660254037844385966, 1.000000000000000000, 0.8660254037844387076, 1.000000000000000000, 0.8660254037844378194, 1.000000000000000888 ) ) 
 REPRESENTATION_ITEM ( '' )  );
#3913=EDGE_LOOP ( 'NONE', ( #974, #10572, #11415, #10187 ) ) ;
#3916=LINE ( 'NONE', #8936, #3319 ) ;
#3931=EDGE_CURVE ( 'NONE', #451, #12353, #798, .T. ) ;
#3933=CARTESIAN_POINT ( 'NONE',  ( 3.800000000000015365, 90.00000000000000000, 3.312500001229034652 ) ) ;
#3951=EDGE_LOOP ( 'NONE', ( #7018, #6032, #5943, #8314 ) ) ;
#3959=PLANE ( 'NONE',  #3072 ) ;
#3962=CARTESIAN_POINT ( 'NONE',  ( 66.44356964374999563, 71.84604660189820891, 3.246875000614517059 ) ) ;
#3993=CARTESIAN_POINT ( 'NONE',  ( 3.591865698314129496, 91.49237114305354623, 2.999999999999999556 ) ) ;
#3996=ORIENTED_EDGE ( 'NONE', *, *, #7915, .F. ) ;
#4004=VECTOR ( 'NONE', #5626, 1000.000000000000000 ) ;
#4008=CARTESIAN_POINT ( 'NONE',  ( 50.72178482187501203, 62.76906990284730625, 4.503125000614517148 ) ) ;
#4018=CARTESIAN_POINT ( 'NONE',  ( 43.37907491812715932, 120.1818777491212700, 3.000000000000001332 ) ) ;
#4024=ADVANCED_FACE ( 'NONE', ( #8920 ), #3959, .T. ) ;
#4026=CARTESIAN_POINT ( 'NONE',  ( 66.44356964374999563, 90.00000000000000000, 4.184375000614516615 ) ) ;
#4061=CARTESIAN_POINT ( 'NONE',  ( 19.27821517812500574, 117.2309300971526937, 4.278125000614516615 ) ) ;
#4070=CARTESIAN_POINT ( 'NONE',  ( 35.00000000000000000, 126.3079067962036106, 4.240625000614517859 ) ) ;
#4075=CARTESIAN_POINT ( 'NONE',  ( 3.800000000000055334, 71.98667160128364628, 4.137500000000000178 ) ) ;
#4080=CARTESIAN_POINT ( 'NONE',  ( 54.68276421697586187, 114.3044457306839234, 3.000000000000001332 ) ) ;
#4088=CARTESIAN_POINT ( 'NONE',  ( 19.27821517812500574, 117.2309300971526937, 2.984375000614517326 ) ) ;
#4093=EDGE_CURVE ( 'NONE', #12605, #11420, #6845, .T. ) ;
#4111=CARTESIAN_POINT ( 'NONE',  ( 3.800000000000015365, 90.00000000000000000, 3.650000000000000355 ) ) ;
#4128=PRODUCT_CONTEXT ( 'NONE', #7514, 'mechanical' ) ;
#4129=CARTESIAN_POINT ( 'NONE',  ( 19.27821517812500574, 117.2309300971526937, 3.378125000614517148 ) ) ;
#4134=CARTESIAN_POINT ( 'NONE',  ( 35.00000000000000000, 90.00000000000000000, 6.000000000000000000 ) ) ;
#4152=CARTESIAN_POINT ( 'NONE',  ( 35.00000000000000711, 53.69209320379640360, 3.621875000614517059 ) ) ;
#4161=EDGE_CURVE ( 'NONE', #12628, #11494, #3702, .T. ) ;
#4168=ORIENTED_EDGE ( 'NONE', *, *, #10496, .T. ) ;
#4170=VECTOR ( 'NONE', #4673, 1000.000000000000000 ) ;
#4178=DIRECTION ( 'NONE',  ( 0.000000000000000000, 0.000000000000000000, 1.000000000000000000 ) ) ;
#4179=ORIENTED_EDGE ( 'NONE', *, *, #10241, .F. ) ;
#4186=CARTESIAN_POINT ( 'NONE',  ( 35.00000000000000000, 90.00000000000000000, 6.000000000000000000 ) ) ;
#4193=CARTESIAN_POINT ( 'NONE',  ( 35.00000000000000000, 126.0266567974326222, 4.550000001229034474 ) ) ;
#4200=CARTESIAN_POINT ( 'NONE',  ( 35.00000000000000000, 126.3079067962036106, 3.790625000614517237 ) ) ;
#4223=CARTESIAN_POINT ( 'NONE',  ( 3.800000000000004707, 90.00000000000000000, 6.000000000000000000 ) ) ;
#4226=AXIS2_PLACEMENT_3D ( 'NONE', #5936, #3004, #6986 ) ;
#4228=EDGE_CURVE ( 'NONE', #11619, #12205, #4748, .T. ) ;
#4230=CARTESIAN_POINT ( 'NONE',  ( 50.72178482187501203, 62.76906990284730625, 3.209375000614517415 ) ) ;
#4234=ORIENTED_EDGE ( 'NONE', *, *, #11049, .F. ) ;
#4255=CARTESIAN_POINT ( 'NONE',  ( 33.50000000000000711, 79.80000000000001137, 8.000000000000000000 ) ) ;
#4259=CARTESIAN_POINT ( 'NONE',  ( 50.72178482187501203, 62.76906990284730625, 3.153125000614517504 ) ) ;
#4263=ORIENTED_EDGE ( 'NONE', *, *, #8751, .T. ) ;
#4295=CARTESIAN_POINT ( 'NONE',  ( 19.27821517812500574, 117.2309300971526937, 3.434375000614517059 ) ) ;
#4303=DIRECTION ( 'NONE',  ( -0.000000000000000000, -0.000000000000000000, -1.000000000000000000 ) ) ;
#4321=CARTESIAN_POINT ( 'NONE',  ( 3.556430356250014579, 108.1539533981018053, 4.765625000614517326 ) ) ;
#4345=EDGE_CURVE ( 'NONE', #10785, #12605, #4821, .T. ) ;
#4383=ORIENTED_EDGE ( 'NONE', *, *, #4161, .F. ) ;
#4384=CARTESIAN_POINT ( 'NONE',  ( 56.62812188930148949, 112.6043444984596533, 3.000000000000000000 ) ) ;
#4395=EDGE_CURVE ( 'NONE', #9287, #8977, #5660, .T. ) ;
#4401=VECTOR ( 'NONE', #8346, 1000.000000000000000 ) ;
#4403=CARTESIAN_POINT ( 'NONE',  ( 66.44356964374999563, 90.00000000000000000, 3.284375000614517148 ) ) ;
#4407=CARTESIAN_POINT ( 'NONE',  ( 4.030338320500828075, 95.53249351899766850, 2.999999999999999556 ) ) ;
#4421=ORIENTED_EDGE ( 'NONE', *, *, #7379, .F. ) ;
#4428=CARTESIAN_POINT ( 'NONE',  ( 66.19999999999988916, 71.98667160128361786, 4.400000001229033231 ) ) ;
#4432=EDGE_CURVE ( 'NONE', #12789, #12512, #8497, .T. ) ;
#4442=VERTEX_POINT ( 'NONE', #3527 ) ;
#4443=EDGE_CURVE ( 'NONE', #10977, #12789, #12484, .T. ) ;
#4464=CARTESIAN_POINT ( 'NONE',  ( 19.27821517812500574, 117.2309300971526937, 2.984375000614517326 ) ) ;
#4468=CARTESIAN_POINT ( 'NONE',  ( 13.53859087060910404, 112.9805567844265539, 2.999999999999999112 ) ) ;
#4499=CIRCLE ( 'NONE', #2206, 31.20000000000000639 ) ;
#4518=VECTOR ( 'NONE', #1529, 1000.000000000000000 ) ;
#4524=CARTESIAN_POINT ( 'NONE',  ( 31.55032196868182126, 58.90710318828558911, 3.000000000000000444 ) ) ;
#4547=CARTESIAN_POINT ( 'NONE',  ( 19.40000000000000924, 117.0199925980744666, 3.575000000000000178 ) ) ;
#4555=CARTESIAN_POINT ( 'NONE',  ( 66.20000000000000284, 90.00000000000000000, 6.000000000000000000 ) ) ;
#4558=CARTESIAN_POINT ( 'NONE',  ( 66.19999999999988916, 71.98667160128361786, 3.050000001229034030 ) ) ;
#4580=CARTESIAN_POINT ( 'NONE',  ( 3.800000000000015810, 108.0133283987162969, 4.625000001229034652 ) ) ;
#4587=CARTESIAN_POINT ( 'NONE',  ( 14.31119263734989033, 66.46175970803329847, 3.000000000000000444 ) ) ;
#4598=CARTESIAN_POINT ( 'NONE',  ( 35.00000000000000000, 126.3079067962035822, 3.396875000614517415 ) ) ;
#4603=CARTESIAN_POINT ( 'NONE',  ( 12.08740047754302616, 111.5578937668422270, 3.000000000000000888 ) ) ;
#4613=LINE ( 'NONE', #1728, #4518 ) ;
#4618=CARTESIAN_POINT ( 'NONE',  ( 35.00000000000000711, 53.97334320256736362, 3.762500000000000178 ) ) ;
#4622=DIRECTION ( 'NONE',  ( -0.000000000000000000, -0.000000000000000000, -1.000000000000000000 ) ) ;
#4645=CARTESIAN_POINT ( 'NONE',  ( 66.19999999999997442, 108.0133283987163253, 3.125000001229034208 ) ) ;
#4657=ORIENTED_EDGE ( 'NONE', *, *, #3785, .T. ) ;
#4661=ORIENTED_EDGE ( 'NONE', *, *, #4687, .T. ) ;
#4662=CARTESIAN_POINT ( 'NONE',  ( 19.27821517812503060, 62.76906990284727783, 4.484375000614516438 ) ) ;
#4673=DIRECTION ( 'NONE',  ( -0.000000000000000000, -0.000000000000000000, -1.000000000000000000 ) ) ;
#4680=CARTESIAN_POINT ( 'NONE',  ( 66.19999999999997442, 108.0133283987163253, 3.462499999999999911 ) ) ;
#4687=EDGE_CURVE ( 'NONE', #5750, #4968, #3121, .T. ) ;
#4712=ORIENTED_EDGE ( 'NONE', *, *, #11454, .T. ) ;
#4717=CARTESIAN_POINT ( 'NONE',  ( 9.181393010286774015, 72.18334839091693311, 3.000000000000002220 ) ) ;
#4718=CARTESIAN_POINT ( 'NONE',  ( 35.00000000000000711, 53.97334320256736362, 3.312500000000000000 ) ) ;
#4727=CARTESIAN_POINT ( 'NONE',  ( 3.556430356250028790, 71.84604660189818048, 3.040625000614517237 ) ) ;
#4730=CARTESIAN_POINT ( 'NONE',  ( 50.59999999999999432, 117.0199925980744666, 3.950000000000000178 ) ) ;
#4740=DIRECTION ( 'NONE',  ( 0.000000000000000000, -1.000000000000000000, 0.000000000000000000 ) ) ;
#4744=CARTESIAN_POINT ( 'NONE',  ( 3.800000000000025135, 71.98667160128366049, 4.137500000000001066 ) ) ;
#4748=( BOUNDED_CURVE ( )  B_SPLINE_CURVE ( 2, ( #11721, #7670, #12899, #11850, #4730, #8715, #6875 ),
 .UNSPECIFIED., .F., .F. ) 
 B_SPLINE_CURVE_WITH_KNOTS ( ( 3, 2, 2, 3 ),
 ( 0.3999999999999999667, 0.4333333333333333481, 0.4666666666666667296, 0.5000000000000001110 ),
 .UNSPECIFIED. ) 
 CURVE ( )  GEOMETRIC_REPRESENTATION_ITEM ( )  RATIONAL_B_SPLINE_CURVE ( ( 1.000000000000000444, 0.8660254037844385966, 1.000000000000000000, 0.8660254037844387076, 1.000000000000000000, 0.8660254037844382635, 1.000000000000000444 ) ) 
 REPRESENTATION_ITEM ( '' )  );
#4756=CARTESIAN_POINT ( 'NONE',  ( 35.00000000000000711, 53.69209320379639649, 4.521875000614516971 ) ) ;
#4779=CARTESIAN_POINT ( 'NONE',  ( 3.557912590344627368, 88.92516271332206657, 3.000000000000001776 ) ) ;
#4780=LINE ( 'NONE', #5820, #6861 ) ;
#4784=CARTESIAN_POINT ( 'NONE',  ( 3.556430356250015024, 90.00000000000000000, 4.803125000614516971 ) ) ;
#4787=CARTESIAN_POINT ( 'NONE',  ( 50.72178482187499071, 117.2309300971526937, 4.203125000614517326 ) ) ;
#4808=CARTESIAN_POINT ( 'NONE',  ( 35.00000000000000000, 126.0266567974326222, 3.987499999999999378 ) ) ;
#4819=CARTESIAN_POINT ( 'NONE',  ( 3.556430356250015024, 90.00000000000000000, 3.959375000614517415 ) ) ;
#4821=( BOUNDED_CURVE ( )  B_SPLINE_CURVE ( 2, ( #12107, #979, #51, #9158, #2039, #6145, #2172, #8059, #4008, #9225, #8187, #6018, #10014, #3222, #7203, #4070, #183, #11190, #12043, #1109, #1178, #10141, #3157, #7990, #11975, #4979, #5169, #4200, #12174, #2959, #7135, #2243, #6218, #10209, #6939, #3090, #11117, #1246, #1975, #5238, #10986, #7070, #428, #9029, #10924, #11052, #120, #2107, #5101, #3020, #1045 ),
 .UNSPECIFIED., .F., .F. ) 
 B_SPLINE_CURVE_WITH_KNOTS ( ( 3, 2, 2, 2, 2, 2, 2, 2, 2, 2, 2, 2, 2, 2, 2, 2, 2, 2, 2, 2, 2, 2, 2, 2, 2, 3 ),
 ( 0.000000000000000000, 0.03333333333333333287, 0.06666666666666666574, 0.1000000000000000194, 0.1333333333333333315, 0.1666666666666666574, 0.2000000000000000389, 0.2333333333333333648, 0.2666666666666666630, 0.2999999999999999889, 0.3333333333333333148, 0.3666666666666666408, 0.4000000000000000777, 0.4333333333333333481, 0.4666666666666667296, 0.5000000000000000000, 0.5333333333333333259, 0.5666666666666666519, 0.5999999999999999778, 0.6333333333333331927, 0.6666666666666666297, 0.6999999999999999556, 0.7333333333333332815, 0.7666666666666667185, 0.8000000000000001554, 0.8015729473302189989 ),
 .UNSPECIFIED. ) 
 CURVE ( )  GEOMETRIC_REPRESENTATION_ITEM ( )  RATIONAL_B_SPLINE_CURVE ( ( 1.000000000000000000, 0.8660254037844387076, 1.000000000000000000, 0.8660254037844387076, 1.000000000000000000, 0.8660254037844387076, 1.000000000000000000, 0.8660254037844387076, 1.000000000000000000, 0.8660254037844387076, 1.000000000000000000, 0.8660254037844387076, 1.000000000000000000, 0.8660254037844387076, 1.000000000000000000, 0.8660254037844387076, 1.000000000000000000, 0.8660254037844387076, 1.000000000000000000, 0.8660254037844387076, 1.000000000000000000, 0.8660254037844387076, 1.000000000000000000, 0.8660254037844387076, 1.000000000000000000, 0.8660254037844387076, 1.000000000000000000, 0.8660254037844387076, 1.000000000000000000, 0.8660254037844387076, 1.000000000000000000, 0.8660254037844387076, 1.000000000000000000, 0.8660254037844387076, 1.000000000000000000, 0.8660254037844387076, 1.000000000000000000, 0.8660254037844387076, 1.000000000000000000, 0.8660254037844387076, 1.000000000000000000, 0.8660254037844387076, 1.000000000000000000, 0.8660254037844387076, 1.000000000000000000, 0.8660254037844387076, 1.000000000000000000, 0.8660254037844387076, 1.000000000000000000, 0.9936779504969671661, 0.9879525560471726919 ) ) 
 REPRESENTATION_ITEM ( '' )  );
#4824=DIRECTION ( 'NONE',  ( 0.000000000000000000, 0.000000000000000000, 1.000000000000000000 ) ) ;
#4833=DIRECTION ( 'NONE',  ( -1.000000000000000000, -0.000000000000000000, -0.000000000000000000 ) ) ;
#4840=EDGE_LOOP ( 'NONE', ( #4234, #5007, #4168, #7450 ) ) ;
#4852=CARTESIAN_POINT ( 'NONE',  ( 35.00000000000000000, 126.3079067962035822, 3.340625000614517059 ) ) ;
#4869=CARTESIAN_POINT ( 'NONE',  ( 35.00000000000000711, 53.97334320256736362, 4.212500000000000355 ) ) ;
#4881=CARTESIAN_POINT ( 'NONE',  ( 66.44356964374998142, 108.1539533981018053, 4.221875000614517148 ) ) ;
#4884=ORIENTED_EDGE ( 'NONE', *, *, #10120, .T. ) ;
#4886=DIRECTION ( 'NONE',  ( 1.000000000000000000, 0.000000000000000000, 0.000000000000000000 ) ) ;
#4906=AXIS2_PLACEMENT_3D ( 'NONE', #6688, #5961, #6751 ) ;
#4914=CARTESIAN_POINT ( 'NONE',  ( 50.72178482187501203, 62.76906990284730625, 4.053125000614517859 ) ) ;
#4916=CARTESIAN_POINT ( 'NONE',  ( 3.556430356250015024, 90.00000000000000000, 4.831250000614517148 ) ) ;
#4937=CARTESIAN_POINT ( 'NONE',  ( 3.556430356250014579, 108.1539533981018053, 3.921875000614517326 ) ) ;
#4945=CARTESIAN_POINT ( 'NONE',  ( 50.72178482187499071, 117.2309300971526937, 4.709375000614516971 ) ) ;
#4954=DIRECTION ( 'NONE',  ( 0.000000000000000000, 0.000000000000000000, 1.000000000000000000 ) ) ;
#4968=VERTEX_POINT ( 'NONE', #12917 ) ;
#4974=CARTESIAN_POINT ( 'NONE',  ( 50.72178482187499071, 117.2309300971526937, 4.653125000614517504 ) ) ;
#4979=CARTESIAN_POINT ( 'NONE',  ( 3.556430356250014579, 108.1539533981018053, 3.865625000614517415 ) ) ;
#4984=VERTEX_POINT ( 'NONE', #1927 ) ;
#5006=CARTESIAN_POINT ( 'NONE',  ( 3.556430356250015024, 90.00000000000000000, 4.409375000614517148 ) ) ;
#5007=ORIENTED_EDGE ( 'NONE', *, *, #11742, .F. ) ;
#5033=CARTESIAN_POINT ( 'NONE',  ( 3.556430356250014579, 108.1539533981018053, 3.415625000614517237 ) ) ;
#5044=EDGE_LOOP ( 'NONE', ( #7375, #2638, #9922, #4263, #8890, #2233 ) ) ;
#5050=EDGE_LOOP ( 'NONE', ( #553, #8460, #4712, #3531 ) ) ;
#5055=CARTESIAN_POINT ( 'NONE',  ( 19.27821517812500574, 117.2309300971526937, 3.434375000614517059 ) ) ;
#5064=DIRECTION ( 'NONE',  ( 0.000000000000000000, 1.000000000000000000, 0.000000000000000000 ) ) ;
#5065=CARTESIAN_POINT ( 'NONE',  ( 66.44356964375000985, 71.84604660189820891, 3.246875000614517504 ) ) ;
#5074=CARTESIAN_POINT ( 'NONE',  ( 33.50000000000000711, 67.79999999999999716, 8.000000000000000000 ) ) ;
#5088=ORIENTED_EDGE ( 'NONE', *, *, #8326, .T. ) ;
#5095=CARTESIAN_POINT ( 'NONE',  ( 66.44356964374998142, 108.1539533981018053, 4.165625000614516793 ) ) ;
#5101=CARTESIAN_POINT ( 'NONE',  ( 3.556430356250015024, 90.00000000000000000, 3.003125000614517148 ) ) ;
#5107=ORIENTED_EDGE ( 'NONE', *, *, #7675, .T. ) ;
#5112=CARTESIAN_POINT ( 'NONE',  ( 44.60848457269055700, 119.8079162999732432, 3.000000000000003109 ) ) ;
#5121=CARTESIAN_POINT ( 'NONE',  ( 50.72178482187501203, 62.76906990284730625, 3.659375000614517592 ) ) ;
#5134=CARTESIAN_POINT ( 'NONE',  ( 3.556430356250014579, 103.6582747873649311, 3.031161570002773420 ) ) ;
#5155=ORIENTED_EDGE ( 'NONE', *, *, #12796, .T. ) ;
#5163=CARTESIAN_POINT ( 'NONE',  ( 50.72178482187499071, 117.2309300971526937, 4.653125000614517504 ) ) ;
#5169=CARTESIAN_POINT ( 'NONE',  ( 19.27821517812500574, 117.2309300971526937, 3.828125000614516882 ) ) ;
#5178=ORIENTED_EDGE ( 'NONE', *, *, #11742, .T. ) ;
#5184=DIRECTION ( 'NONE',  ( 0.000000000000000000, -0.000000000000000000, 1.000000000000000000 ) ) ;
#5189=CARTESIAN_POINT ( 'NONE',  ( 3.556430356250015024, 90.00000000000000000, 4.859375000614517326 ) ) ;
#5209=DIRECTION ( 'NONE',  ( -0.000000000000000000, -0.000000000000000000, -1.000000000000000000 ) ) ;
#5230=CARTESIAN_POINT ( 'NONE',  ( 3.556430356250028790, 71.84604660189818048, 3.940625000614518036 ) ) ;
#5235=ORIENTED_EDGE ( 'NONE', *, *, #3128, .F. ) ;
#5236=CIRCLE ( 'NONE', #6687, 31.20000000000000639 ) ;
#5238=CARTESIAN_POINT ( 'NONE',  ( 35.00000000000000000, 126.3079067962036106, 3.340625000614517504 ) ) ;
#5249=ORIENTED_EDGE ( 'NONE', *, *, #10868, .T. ) ;
#5263=CARTESIAN_POINT ( 'NONE',  ( 35.00000000000000000, 90.00000000000000000, 6.000000000000000000 ) ) ;
#5277=FACE_BOUND ( 'NONE', #5044, .T. ) ;
#5287=ADVANCED_BREP_SHAPE_REPRESENTATION ( '', ( #3386, #5704 ), #60 ) ;
#5294=CARTESIAN_POINT ( 'NONE',  ( 60.63303222545420823, 111.5086687406912347, 2.829484441871016109 ) ) ;
#5309=CARTESIAN_POINT ( 'NONE',  ( 35.00000000000000000, 126.0266567974326222, 3.087499999999999911 ) ) ;
#5328=CARTESIAN_POINT ( 'NONE',  ( 3.556430356250028790, 71.84604660189818048, 3.546875000614517326 ) ) ;
#5338=AXIS2_PLACEMENT_3D ( 'NONE', #8699, #1568, #11642 ) ;
#5348=MECHANICAL_DESIGN_GEOMETRIC_PRESENTATION_REPRESENTATION('',(#10789),#10982);
#5356=CARTESIAN_POINT ( 'NONE',  ( 19.40000000000000924, 117.0199925980744666, 4.137500001229033941 ) ) ;
#5364=SHAPE_REPRESENTATION_RELATIONSHIP ( 'NONE' , 'NONE' ,  #1066, #5287 ) ;
#5365=VECTOR ( 'NONE', #11626, 1000.000000000000000 ) ;
#5371=CARTESIAN_POINT ( 'NONE',  ( 35.00000000000000711, 53.69209320379640360, 4.521875000614516971 ) ) ;
#5399=ORIENTED_EDGE ( 'NONE', *, *, #3059, .F. ) ;
#5420=CARTESIAN_POINT ( 'NONE',  ( 3.800000000000015365, 108.0133283987163111, 2.825000001229034385 ) ) ;
#5446=AXIS2_PLACEMENT_3D ( 'NONE', #394, #8397, #5184 ) ;
#5460=DIRECTION ( 'NONE',  ( -1.000000000000000000, 0.000000000000000000, 0.000000000000000000 ) ) ;
#5461=CARTESIAN_POINT ( 'NONE',  ( 19.40000000000002700, 62.98000740192551206, 4.625000000000000000 ) ) ;
#5489=DIRECTION ( 'NONE',  ( 1.000000000000000000, 0.000000000000000000, 0.000000000000000000 ) ) ;
#5491=CARTESIAN_POINT ( 'NONE',  ( 32.83880403052557284, 58.79641609890851583, 3.000000000000001776 ) ) ;
#5504=CARTESIAN_POINT ( 'NONE',  ( 66.44356964374999563, 90.00000000000000000, 4.634375000614516793 ) ) ;
#5522=ORIENTED_EDGE ( 'NONE', *, *, #10037, .T. ) ;
#5532=FACE_OUTER_BOUND ( 'NONE', #7173, .T. ) ;
#5533=ORIENTED_EDGE ( 'NONE', *, *, #9064, .F. ) ;
#5554=CARTESIAN_POINT ( 'NONE',  ( 19.40000000000000924, 117.0199925980744666, 3.687500001229034208 ) ) ;
#5559=AXIS2_PLACEMENT_3D ( 'NONE', #6063, #2287, #7116 ) ;
#5571=EDGE_LOOP ( 'NONE', ( #5235, #10195, #9629, #2186 ) ) ;
#5572=CARTESIAN_POINT ( 'NONE',  ( 66.44356964374999563, 71.84604660189820891, 3.696875000614517237 ) ) ;
#5575=CARTESIAN_POINT ( 'NONE',  ( 7.321936442954655178, 105.0558282920940627, 3.000000000000000444 ) ) ;
#5589=CARTESIAN_POINT ( 'NONE',  ( 66.19999999999998863, 90.00000000000000000, 3.425000000000000266 ) ) ;
#5592=CARTESIAN_POINT ( 'NONE',  ( 66.19999999999998863, 90.00000000000000000, 4.325000000000000178 ) ) ;
#5599=CARTESIAN_POINT ( 'NONE',  ( 50.60000000000001563, 62.98000740192552627, 3.012500001229034829 ) ) ;
#5621=CARTESIAN_POINT ( 'NONE',  ( 19.40000000000000924, 117.0199925980744666, 3.237500001229034030 ) ) ;
#5626=DIRECTION ( 'NONE',  ( -0.000000000000000000, -0.000000000000000000, -1.000000000000000000 ) ) ;
#5629=CARTESIAN_POINT ( 'NONE',  ( 44.79423261070191131, 60.36750792639232799, 3.000000000000000444 ) ) ;
#5638=CARTESIAN_POINT ( 'NONE',  ( 3.556430356250014579, 108.1539533981018053, 4.821875000614516793 ) ) ;
#5640=EDGE_CURVE ( 'NONE', #10525, #4968, #6995, .T. ) ;
#5653=CARTESIAN_POINT ( 'NONE',  ( 3.556430356250015024, 90.00000000000000000, 4.803125000614516971 ) ) ;
#5656=CARTESIAN_POINT ( 'NONE',  ( 50.59999999999999432, 117.0199925980744666, 3.500000000000000444 ) ) ;
#5660=( BOUNDED_CURVE ( )  B_SPLINE_CURVE ( 2, ( #8622, #757, #6520, #8685, #2673, #10515, #12613 ),
 .UNSPECIFIED., .F., .F. ) 
 B_SPLINE_CURVE_WITH_KNOTS ( ( 3, 2, 2, 3 ),
 ( 0.1999999999999999833, 0.2333333333333333925, 0.2666666666666668295, 0.3000000000000002109 ),
 .UNSPECIFIED. ) 
 CURVE ( )  GEOMETRIC_REPRESENTATION_ITEM ( )  RATIONAL_B_SPLINE_CURVE ( ( 1.000000000000000222, 0.8660254037844385966, 1.000000000000000000, 0.8660254037844387076, 1.000000000000000000, 0.8660254037844378194, 1.000000000000000888 ) ) 
 REPRESENTATION_ITEM ( '' )  );
#5661=CARTESIAN_POINT ( 'NONE',  ( 35.00000000000000000, 90.00000000000000000, 6.000000000000000000 ) ) ;
#5682=CARTESIAN_POINT ( 'NONE',  ( 35.00000000000000000, 90.00000000000000000, 3.000000000000000000 ) ) ;
#5702=CARTESIAN_POINT ( 'NONE',  ( 19.27821517812503060, 62.76906990284727783, 3.078125000614517326 ) ) ;
#5703=ORIENTED_EDGE ( 'NONE', *, *, #7274, .T. ) ;
#5704=AXIS2_PLACEMENT_3D ( 'NONE', #8997, #4824, #4886 ) ;
#5709=EDGE_CURVE ( 'NONE', #7460, #8977, #4780, .T. ) ;
#5720=CARTESIAN_POINT ( 'NONE',  ( 3.800000000000015365, 90.00000000000000000, 4.100000000000000533 ) ) ;
#5750=VERTEX_POINT ( 'NONE', #3933 ) ;
#5760=CARTESIAN_POINT ( 'NONE',  ( 35.00000000000000000, 90.00000000000000000, 3.000000000000000000 ) ) ;
#5763=FACE_OUTER_BOUND ( 'NONE', #2688, .T. ) ;
#5784=CARTESIAN_POINT ( 'NONE',  ( 35.00000000000000711, 53.97334320256736362, 4.662499999999999645 ) ) ;
#5810=LINE ( 'NONE', #27, #304 ) ;
#5820=CARTESIAN_POINT ( 'NONE',  ( 66.20000000000000284, 90.00000000000000000, 6.000000000000000000 ) ) ;
#5828=CARTESIAN_POINT ( 'NONE',  ( 66.44356964374999563, 71.84604660189820891, 4.540625000614517681 ) ) ;
#5846=CARTESIAN_POINT ( 'NONE',  ( 36.50000000000001421, 67.79999999999999716, 6.000000000000000000 ) ) ;
#5860=VERTEX_POINT ( 'NONE', #9079 ) ;
#5863=DIRECTION ( 'NONE',  ( -0.000000000000000000, -0.000000000000000000, -1.000000000000000000 ) ) ;
#5875=ORIENTED_EDGE ( 'NONE', *, *, #6796, .F. ) ;
#5886=CARTESIAN_POINT ( 'NONE',  ( 66.44356964374999563, 90.00000000000000000, 3.678125000614516971 ) ) ;
#5894=ADVANCED_FACE ( 'NONE', ( #7978 ), #167, .F. ) ;
#5907=CARTESIAN_POINT ( 'NONE',  ( 66.44356964374998142, 108.1539533981018053, 4.221875000614517148 ) ) ;
#5919=VECTOR ( 'NONE', #4303, 1000.000000000000000 ) ;
#5936=CARTESIAN_POINT ( 'NONE',  ( 35.00000000000000000, 90.00000000000000000, 6.000000000000000000 ) ) ;
#5943=ORIENTED_EDGE ( 'NONE', *, *, #2283, .F. ) ;
#5949=CARTESIAN_POINT ( 'NONE',  ( 3.556430356250014579, 108.1539533981018053, 4.765625000614517326 ) ) ;
#5961=DIRECTION ( 'NONE',  ( -0.000000000000000000, -0.000000000000000000, -1.000000000000000000 ) ) ;
#5963=CARTESIAN_POINT ( 'NONE',  ( 18.66882170374126915, 116.8715781131384688, 3.000000000000000000 ) ) ;
#5973=CARTESIAN_POINT ( 'NONE',  ( 19.27821517812503060, 62.76906990284727783, 3.134375000614517237 ) ) ;
#6010=CARTESIAN_POINT ( 'NONE',  ( 3.556430356250015024, 90.00000000000000000, 4.353125000614517681 ) ) ;
#6018=CARTESIAN_POINT ( 'NONE',  ( 3.556430356250028790, 71.84604660189818048, 4.390625000614517326 ) ) ;
#6019=CARTESIAN_POINT ( 'NONE',  ( 35.00000000000000000, 126.0266567974326222, 4.887499999999999289 ) ) ;
#6028=CARTESIAN_POINT ( 'NONE',  ( 55.18046915913835448, 113.8894995096903955, 3.000000000000000888 ) ) ;
#6032=ORIENTED_EDGE ( 'NONE', *, *, #422, .F. ) ;
#6038=CARTESIAN_POINT ( 'NONE',  ( 3.556430356250028790, 71.84604660189818048, 3.996875000614517059 ) ) ;
#6061=DIRECTION ( 'NONE',  ( -0.000000000000000000, -0.000000000000000000, -1.000000000000000000 ) ) ;
#6062=VERTEX_POINT ( 'NONE', #12291 ) ;
#6063=CARTESIAN_POINT ( 'NONE',  ( 35.00000000000000000, 90.00000000000000000, 6.000000000000000000 ) ) ;
#6078=CARTESIAN_POINT ( 'NONE',  ( 66.44356964374999563, 90.00000000000000000, 3.228125000614517237 ) ) ;
#6082=EDGE_LOOP ( 'NONE', ( #12567, #11047 ) ) ;
#6092=CARTESIAN_POINT ( 'NONE',  ( 40.89629752784551897, 120.7937367018730725, 3.000000000000000000 ) ) ;
#6100=CARTESIAN_POINT ( 'NONE',  ( 50.72178482187499071, 117.2309300971526937, 3.809375000614517504 ) ) ;
#6136=SHAPE_DEFINITION_REPRESENTATION ( #9283, #1066 ) ;
#6137=CARTESIAN_POINT ( 'NONE',  ( 50.59999999999999432, 117.0199925980744666, 4.512500001229033941 ) ) ;
#6145=CARTESIAN_POINT ( 'NONE',  ( 66.44356964374998142, 108.1539533981018053, 4.615625000614516971 ) ) ;
#6163=EDGE_LOOP ( 'NONE', ( #3407, #7657, #9803, #10497 ) ) ;
#6168=CARTESIAN_POINT ( 'NONE',  ( 64.31840934454761793, 100.6710296366163249, 2.999476389609550431 ) ) ;
#6188=CARTESIAN_POINT ( 'NONE',  ( 66.20000000000008811, 108.0133283987162542, 4.025000001229034119 ) ) ;
#6191=EDGE_LOOP ( 'NONE', ( #7976, #11412, #456, #8443 ) ) ;
#6205=PRODUCT_DEFINITION_CONTEXT ( 'detailed design', #8533, 'design' ) ;
#6211=CARTESIAN_POINT ( 'NONE',  ( 35.00000000000000711, 53.69209320379640360, 4.015625000614517326 ) ) ;
#6218=CARTESIAN_POINT ( 'NONE',  ( 50.72178482187501203, 62.76906990284730625, 3.603125000614517681 ) ) ;
#6222=( LENGTH_UNIT ( ) NAMED_UNIT ( * ) SI_UNIT ( .MILLI., .METRE. ) );
#6242=LINE ( 'NONE', #6624, #4170 ) ;
#6246=CARTESIAN_POINT ( 'NONE',  ( 3.556430356250015024, 90.00000000000000000, 3.059375000614517059 ) ) ;
#6253=CARTESIAN_POINT ( 'NONE',  ( 19.40000000000000924, 117.0199925980744666, 4.137500001229033941 ) ) ;
#6276=CARTESIAN_POINT ( 'NONE',  ( 3.556430356250028790, 71.84604660189818048, 3.040625000614517237 ) ) ;
#6277=ORIENTED_EDGE ( 'NONE', *, *, #4432, .T. ) ;
#6297=CIRCLE ( 'NONE', #218, 31.20000000000000639 ) ;
#6309=CARTESIAN_POINT ( 'NONE',  ( 50.72178482187501203, 62.76906990284730625, 3.659375000614517592 ) ) ;
#6315=DIRECTION ( 'NONE',  ( -0.000000000000000000, -0.000000000000000000, -1.000000000000000000 ) ) ;
#6321=ORIENTED_EDGE ( 'NONE', *, *, #12182, .F. ) ;
#6335=CARTESIAN_POINT ( 'NONE',  ( 35.00000000000000000, 126.0266567974326222, 2.750000001229033764 ) ) ;
#6354=CARTESIAN_POINT ( 'NONE',  ( 19.27821517812500574, 117.2309300971526937, 4.334375000614516971 ) ) ;
#6356=ORIENTED_EDGE ( 'NONE', *, *, #300, .T. ) ;
#6400=CARTESIAN_POINT ( 'NONE',  ( 53.66639336120024950, 115.0996716663835571, 3.000000000000001776 ) ) ;
#6402=CARTESIAN_POINT ( 'NONE',  ( 3.800000000000015365, 90.00000000000000000, 3.762500001229034385 ) ) ;
#6417=CARTESIAN_POINT ( 'NONE',  ( 50.72178482187501203, 62.76906990284730625, 3.659375000614517592 ) ) ;
#6421=CARTESIAN_POINT ( 'NONE',  ( 10.74370178410656962, 110.0340209993050706, 3.000000000000000888 ) ) ;
#6425=ADVANCED_FACE ( 'NONE', ( #1592 ), #8467, .F. ) ;
#6444=CARTESIAN_POINT ( 'NONE',  ( 66.19999999999998863, 90.00000000000000000, 4.774999999999999467 ) ) ;
#6454=CARTESIAN_POINT ( 'NONE',  ( 33.50000000000000711, 67.79999999999999716, 6.000000000000000000 ) ) ;
#6457=CARTESIAN_POINT ( 'NONE',  ( 19.40000000000002700, 62.98000740192551206, 3.837500001229034563 ) ) ;
#6465=VERTEX_POINT ( 'NONE', #3564 ) ;
#6468=CARTESIAN_POINT ( 'NONE',  ( 3.800000000000015365, 108.0133283987163111, 3.275000001229034119 ) ) ;
#6472=ORIENTED_EDGE ( 'NONE', *, *, #4228, .F. ) ;
#6477=VECTOR ( 'NONE', #6061, 1000.000000000000000 ) ;
#6520=CARTESIAN_POINT ( 'NONE',  ( 19.40000000000000924, 117.0199925980744666, 4.474999999999999645 ) ) ;
#6533=CARTESIAN_POINT ( 'NONE',  ( 3.800000000000025135, 71.98667160128366049, 3.350000001229034297 ) ) ;
#6539=CARTESIAN_POINT ( 'NONE',  ( 22.35108503858844031, 61.36708817440415942, 3.000000000000000888 ) ) ;
#6549=CARTESIAN_POINT ( 'NONE',  ( 3.556430356250028790, 71.84604660189818048, 3.096875000614517592 ) ) ;
#6553=CARTESIAN_POINT ( 'NONE',  ( 3.640153284139971746, 92.50862168353172876, 3.000000000000000000 ) ) ;
#6566=CARTESIAN_POINT ( 'NONE',  ( 66.19999999999998863, 90.00000000000000000, 3.537500001229034297 ) ) ;
#6588=VECTOR ( 'NONE', #5209, 1000.000000000000000 ) ;
#6597=CARTESIAN_POINT ( 'NONE',  ( 3.800000000000015365, 90.00000000000000000, 3.312500001229034652 ) ) ;
#6604=CARTESIAN_POINT ( 'NONE',  ( 4.452487237934602327, 82.57917759402269553, 2.999999999999998668 ) ) ;
#6614=CARTESIAN_POINT ( 'NONE',  ( 50.72178482187499071, 117.2309300971526937, 3.359375000614517326 ) ) ;
#6624=CARTESIAN_POINT ( 'NONE',  ( 67.70000000000001705, 90.00000000000000000, 6.000000000000000000 ) ) ;
#6633=CARTESIAN_POINT ( 'NONE',  ( 50.59999999999999432, 117.0199925980744666, 3.950000000000000178 ) ) ;
#6638=FACE_OUTER_BOUND ( 'NONE', #8711, .T. ) ;
#6669=CARTESIAN_POINT ( 'NONE',  ( 12.43081896414492782, 68.21485176374228843, 3.000000000000000888 ) ) ;
#6670=CARTESIAN_POINT ( 'NONE',  ( 3.800000000000015365, 90.00000000000000000, 3.200000000000000178 ) ) ;
#6678=CARTESIAN_POINT ( 'NONE',  ( 19.27821517812500574, 117.2309300971526937, 3.378125000614517148 ) ) ;
#6680=AXIS2_PLACEMENT_3D ( 'NONE', #9269, #9335, #9397 ) ;
#6687=AXIS2_PLACEMENT_3D ( 'NONE', #5263, #9253, #276 ) ;
#6688=CARTESIAN_POINT ( 'NONE',  ( 35.00000000000000000, 90.00000000000000000, 6.000000000000000000 ) ) ;
#6697=CARTESIAN_POINT ( 'NONE',  ( 19.40000000000000924, 117.0199925980744666, 3.125000000000000000 ) ) ;
#6704=CARTESIAN_POINT ( 'NONE',  ( 45.39999948872177526, 60.58435772187547030, 2.999999999999999556 ) ) ;
#6710=CARTESIAN_POINT ( 'NONE',  ( 50.72178482187501203, 62.76906990284730625, 4.559375000614517504 ) ) ;
#6711=VERTEX_POINT ( 'NONE', #8469 ) ;
#6720=EDGE_CURVE ( 'NONE', #6465, #4984, #2386, .T. ) ;
#6731=CARTESIAN_POINT ( 'NONE',  ( 42.32262610911597278, 59.65151212041654105, 2.999999999999999556 ) ) ;
#6750=COLOUR_RGB ( '',0.8941176470588234615, 0.8941176470588234615, 0.8941176470588234615 ) ;
#6751=DIRECTION ( 'NONE',  ( -1.000000000000000000, 0.000000000000000000, 0.000000000000000000 ) ) ;
#6759=FACE_OUTER_BOUND ( 'NONE', #9777, .T. ) ;
#6760=B_SPLINE_CURVE_WITH_KNOTS ( 'NONE', 3,
 ( #2776, #7999, #2967, #795 ),
 .UNSPECIFIED., .F., .F.,
 ( 4, 4 ),
 ( 0.000000000000000000, 1.000000000000000000 ),
 .UNSPECIFIED. ) ;
#6764=CARTESIAN_POINT ( 'NONE',  ( 66.20000000000000284, 71.98667160128370313, 3.837500000000000799 ) ) ;
#6776=CARTESIAN_POINT ( 'NONE',  ( 3.556430356250028790, 71.84604660189818048, 3.996875000614517504 ) ) ;
#6782=CARTESIAN_POINT ( 'NONE',  ( 35.00000000000000000, 90.00000000000000000, 3.000000000000000000 ) ) ;
#6793=CYLINDRICAL_SURFACE ( 'NONE', #4226, 31.19999999999999929 ) ;
#6796=EDGE_CURVE ( 'NONE', #8545, #6062, #2517, .T. ) ;
#6807=CARTESIAN_POINT ( 'NONE',  ( 50.72178482187501203, 62.76906990284730625, 4.503125000614517148 ) ) ;
#6825=CARTESIAN_POINT ( 'NONE',  ( 19.40000000000002700, 62.98000740192551206, 3.725000000000000089 ) ) ;
#6826=EDGE_CURVE ( 'NONE', #10249, #8545, #10808, .T. ) ;
#6831=CARTESIAN_POINT ( 'NONE',  ( 3.800000000000004707, 90.00000000000000000, 6.000000000000000000 ) ) ;
#6836=( BOUNDED_CURVE ( )  B_SPLINE_CURVE ( 2, ( #12429, #4580, #3475, #7456, #3539, #11440, #9480 ),
 .UNSPECIFIED., .F., .F. ) 
 B_SPLINE_CURVE_WITH_KNOTS ( ( 3, 2, 2, 3 ),
 ( 0.000000000000000000, 0.03333333333333339532, 0.06666666666666679064, 0.1000000000000001860 ),
 .UNSPECIFIED. ) 
 CURVE ( )  GEOMETRIC_REPRESENTATION_ITEM ( )  RATIONAL_B_SPLINE_CURVE ( ( 1.000000000000000000, 0.8660254037844387076, 1.000000000000000000, 0.8660254037844387076, 1.000000000000000000, 0.8660254037844380415, 1.000000000000000666 ) ) 
 REPRESENTATION_ITEM ( '' )  );
#6845=B_SPLINE_CURVE_WITH_KNOTS ( 'NONE', 3,
 ( #395, #6553, #528, #4407, #1519, #9504, #10288, #11397, #10357, #1321, #5575, #332, #8529, #6421, #4603, #8594, #4468 ),
 .UNSPECIFIED., .F., .F.,
 ( 4, 2, 1, 2, 2, 2, 2, 2, 4 ),
 ( 0.000000000000000000, 0.003052186405622107652, 0.006104372811244215304, 0.009156559216866321654, 0.01068265241967737700, 0.01220874562248843061, 0.01831311843373264331, 0.02136530483935476787, 0.02441749124497688897 ),
 .UNSPECIFIED. ) ;
#6861=VECTOR ( 'NONE', #10664, 1000.000000000000000 ) ;
#6863=CARTESIAN_POINT ( 'NONE',  ( 50.60000000000001563, 62.98000740192552627, 3.350000000000000533 ) ) ;
#6872=CARTESIAN_POINT ( 'NONE',  ( 19.27821517812500574, 117.2309300971526937, 2.928125000614517415 ) ) ;
#6875=CARTESIAN_POINT ( 'NONE',  ( 66.19999999999998863, 90.00000000000000000, 3.875000000000000000 ) ) ;
#6894=CARTESIAN_POINT ( 'NONE',  ( 19.27821517812503060, 62.76906990284727783, 4.034375000614517148 ) ) ;
#6905=ORIENTED_EDGE ( 'NONE', *, *, #11049, .T. ) ;
#6913=( BOUNDED_CURVE ( )  B_SPLINE_CURVE ( 2, ( #8036, #98, #3066, #11031, #2083, #10052, #4111 ),
 .UNSPECIFIED., .F., .F. ) 
 B_SPLINE_CURVE_WITH_KNOTS ( ( 3, 2, 2, 3 ),
 ( 0.5000000000000001110, 0.5333333333333334370, 0.5666666666666666519, 0.5999999999999999778 ),
 .UNSPECIFIED. ) 
 CURVE ( )  GEOMETRIC_REPRESENTATION_ITEM ( )  RATIONAL_B_SPLINE_CURVE ( ( 0.9999999999999995559, 0.8660254037844391517, 1.000000000000000000, 0.8660254037844387076, 1.000000000000000000, 0.8660254037844387076, 1.000000000000000000 ) ) 
 REPRESENTATION_ITEM ( '' )  );
#6936=CARTESIAN_POINT ( 'NONE',  ( 66.44356964374998142, 108.1539533981018053, 3.265625000614516882 ) ) ;
#6939=CARTESIAN_POINT ( 'NONE',  ( 19.27821517812503060, 62.76906990284727783, 3.528125000614517059 ) ) ;
#6956=ORIENTED_EDGE ( 'NONE', *, *, #10868, .F. ) ;
#6957=CARTESIAN_POINT ( 'NONE',  ( 66.44356964374999563, 90.00000000000000000, 4.634375000614516793 ) ) ;
#6962=DIRECTION ( 'NONE',  ( -1.000000000000000000, 0.000000000000000000, 0.000000000000000000 ) ) ;
#6983=EDGE_LOOP ( 'NONE', ( #9888, #2503, #5088, #10312 ) ) ;
#6986=DIRECTION ( 'NONE',  ( -1.000000000000000000, 0.000000000000000000, 0.000000000000000000 ) ) ;
#6990=EDGE_CURVE ( 'NONE', #8977, #11619, #9247, .T. ) ;
#6995=( BOUNDED_CURVE ( )  B_SPLINE_CURVE ( 2, ( #1897, #3680, #6863, #4718, #11646, #3867, #6670 ),
 .UNSPECIFIED., .F., .F. ) 
 B_SPLINE_CURVE_WITH_KNOTS ( ( 3, 2, 2, 3 ),
 ( 0.7000000000000001776, 0.7333333333333335036, 0.7666666666666669405, 0.8000000000000002665 ),
 .UNSPECIFIED. ) 
 CURVE ( )  GEOMETRIC_REPRESENTATION_ITEM ( )  RATIONAL_B_SPLINE_CURVE ( ( 0.9999999999999991118, 0.8660254037844395958, 1.000000000000000000, 0.8660254037844387076, 1.000000000000000000, 0.8660254037844378194, 1.000000000000000888 ) ) 
 REPRESENTATION_ITEM ( '' )  );
#7013=CARTESIAN_POINT ( 'NONE',  ( 66.19999999999998863, 90.00000000000000000, 4.325000000000000178 ) ) ;
#7018=ORIENTED_EDGE ( 'NONE', *, *, #11454, .F. ) ;
#7025=CARTESIAN_POINT ( 'NONE',  ( 35.00000000000000000, 126.3079067962035822, 4.746875000614517504 ) ) ;
#7040=VECTOR ( 'NONE', #1277, 1000.000000000000000 ) ;
#7063=CARTESIAN_POINT ( 'NONE',  ( 3.556430356250014579, 108.1539533981018053, 3.865625000614517415 ) ) ;
#7070=CARTESIAN_POINT ( 'NONE',  ( 66.44356964374998142, 108.1539533981018053, 3.265625000614517326 ) ) ;
#7080=CARTESIAN_POINT ( 'NONE',  ( 35.81220618290669933, 121.3442557591098563, 2.999999999999998668 ) ) ;
#7089=VERTEX_POINT ( 'NONE', #10648 ) ;
#7091=CARTESIAN_POINT ( 'NONE',  ( 3.556430356250028790, 71.84604660189818048, 4.446875000614517681 ) ) ;
#7110=VECTOR ( 'NONE', #5064, 1000.000000000000000 ) ;
#7116=DIRECTION ( 'NONE',  ( -1.000000000000000000, 0.000000000000000000, 0.000000000000000000 ) ) ;
#7119=VERTEX_POINT ( 'NONE', #10522 ) ;
#7124=ADVANCED_FACE ( 'NONE', ( #11756 ), #9297, .F. ) ;
#7129=CARTESIAN_POINT ( 'NONE',  ( 35.00000000000000000, 126.3079067962035822, 4.240625000614517859 ) ) ;
#7134=DIRECTION ( 'NONE',  ( -0.000000000000000000, -0.000000000000000000, -1.000000000000000000 ) ) ;
#7135=CARTESIAN_POINT ( 'NONE',  ( 66.44356964374999563, 90.00000000000000000, 3.678125000614516971 ) ) ;
#7136=CARTESIAN_POINT ( 'NONE',  ( 66.19999999999998863, 90.00000000000000000, 3.875000000000000000 ) ) ;
#7139=CARTESIAN_POINT ( 'NONE',  ( 66.19999999999988916, 71.98667160128361786, 4.287500000000000533 ) ) ;
#7152=CARTESIAN_POINT ( 'NONE',  ( 64.54728993811707483, 100.7543353701752125, 2.858851390224067313 ) ) ;
#7163=CARTESIAN_POINT ( 'NONE',  ( 66.44356964375000985, 71.84604660189820891, 3.696875000614517237 ) ) ;
#7173=EDGE_LOOP ( 'NONE', ( #1542, #8505 ) ) ;
#7186=DIRECTION ( 'NONE',  ( -1.000000000000000000, 0.000000000000000000, 0.000000000000000000 ) ) ;
#7194=CARTESIAN_POINT ( 'NONE',  ( 35.00000000000000711, 53.69209320379640360, 3.565625000614517592 ) ) ;
#7196=CARTESIAN_POINT ( 'NONE',  ( 66.19999999999993179, 71.98667160128364628, 3.500000001229034208 ) ) ;
#7202=VECTOR ( 'NONE', #8506, 1000.000000000000000 ) ;
#7203=CARTESIAN_POINT ( 'NONE',  ( 19.27821517812500574, 117.2309300971526937, 4.278125000614516615 ) ) ;
#7261=CARTESIAN_POINT ( 'NONE',  ( 35.00000000000000711, 53.69209320379640360, 3.115625000614517415 ) ) ;
#7274=EDGE_CURVE ( 'NONE', #7119, #12628, #3916, .T. ) ;
#7276=CIRCLE ( 'NONE', #10194, 31.20000000000000639 ) ;
#7290=CARTESIAN_POINT ( 'NONE',  ( 35.00000000000000000, 90.00000000000000000, 6.000000000000000000 ) ) ;
#7297=CARTESIAN_POINT ( 'NONE',  ( 35.00000000000000000, 126.3079067962036106, 3.396875000614517415 ) ) ;
#7303=CYLINDRICAL_SURFACE ( 'NONE', #2691, 31.19999999999999929 ) ;
#7325=CARTESIAN_POINT ( 'NONE',  ( 35.00000000000000000, 126.0266567974326222, 3.200000001229034385 ) ) ;
#7349=AXIS2_PLACEMENT_3D ( 'NONE', #2689, #5489, #11513 ) ;
#7367=CARTESIAN_POINT ( 'NONE',  ( 3.800000000000039790, 71.98667160128364628, 4.250000001229034652 ) ) ;
#7375=ORIENTED_EDGE ( 'NONE', *, *, #1077, .F. ) ;
#7379=EDGE_CURVE ( 'NONE', #9156, #4442, #7276, .T. ) ;
#7391=( GEOMETRIC_REPRESENTATION_CONTEXT ( 3 ) GLOBAL_UNCERTAINTY_ASSIGNED_CONTEXT ( ( #9174 ) ) GLOBAL_UNIT_ASSIGNED_CONTEXT ( ( #9424, #1310, #12178 ) ) REPRESENTATION_CONTEXT ( 'NONE', 'WORKASPACE' ) );
#7395=ADVANCED_FACE ( 'NONE', ( #11223 ), #7303, .F. ) ;
#7406=CARTESIAN_POINT ( 'NONE',  ( 35.00000000000000000, 126.3079067962035822, 2.946875000614516793 ) ) ;
#7414=CARTESIAN_POINT ( 'NONE',  ( 35.00000000000000000, 90.00000000000000000, 6.000000000000000000 ) ) ;
#7450=ORIENTED_EDGE ( 'NONE', *, *, #10761, .T. ) ;
#7456=CARTESIAN_POINT ( 'NONE',  ( 35.00000000000000000, 126.0266567974326222, 4.550000001229034474 ) ) ;
#7460=VERTEX_POINT ( 'NONE', #8354 ) ;
#7472=CARTESIAN_POINT ( 'NONE',  ( 3.556430356250014579, 108.1539533981018053, 3.921875000614517326 ) ) ;
#7486=DIRECTION ( 'NONE',  ( 0.8660254037844400399, 0.000000000000000000, -0.4999999999999975575 ) ) ;
#7499=CARTESIAN_POINT ( 'NONE',  ( 66.19999999999998863, 90.00000000000000000, 4.437500001229033764 ) ) ;
#7514=APPLICATION_CONTEXT ( 'automotive_design' ) ;
#7524=CARTESIAN_POINT ( 'NONE',  ( 35.00000000000000000, 126.0266567974326222, 3.650000001229034119 ) ) ;
#7531=CARTESIAN_POINT ( 'NONE',  ( 3.939444093506661027, 85.09162761845308864, 3.000000000000000444 ) ) ;
#7538=CARTESIAN_POINT ( 'NONE',  ( 66.44356964374998142, 108.1539533981018053, 3.771875000614516971 ) ) ;
#7561=ADVANCED_FACE ( 'NONE', ( #6638 ), #11417, .T. ) ;
#7567=CARTESIAN_POINT ( 'NONE',  ( 33.50000000000000711, 79.80000000000001137, 8.000000000000000000 ) ) ;
#7575=ADVANCED_FACE ( 'NONE', ( #10441 ), #12401, .F. ) ;
#7585=CARTESIAN_POINT ( 'NONE',  ( 3.800000000000025135, 71.98667160128366049, 2.900000001229034563 ) ) ;
#7591=CARTESIAN_POINT ( 'NONE',  ( 6.084625604134796362, 77.72058018632206711, 2.999999999999999556 ) ) ;
#7602=CARTESIAN_POINT ( 'NONE',  ( 3.556430356250015024, 90.00000000000000000, 4.409375000614517148 ) ) ;
#7612=VECTOR ( 'NONE', #7486, 1000.000000000000227 ) ;
#7614=CARTESIAN_POINT ( 'NONE',  ( 3.678215178125014972, 90.00000000000000000, 4.732812500921776078 ) ) ;
#7627=DIRECTION ( 'NONE',  ( 1.000000000000000000, 0.000000000000000000, -0.000000000000000000 ) ) ;
#7657=ORIENTED_EDGE ( 'NONE', *, *, #9788, .F. ) ;
#7665=EDGE_CURVE ( 'NONE', #1779, #11619, #12539, .T. ) ;
#7667=CARTESIAN_POINT ( 'NONE',  ( 35.00000000000000711, 53.69209320379640360, 4.465625000614517504 ) ) ;
#7670=CARTESIAN_POINT ( 'NONE',  ( 3.799999999999985612, 108.0133283987162827, 4.062500000000000000 ) ) ;
#7675=EDGE_CURVE ( 'NONE', #12353, #10525, #10574, .T. ) ;
#7703=CARTESIAN_POINT ( 'NONE',  ( 3.800000000000015365, 90.00000000000000000, 3.762500001229034385 ) ) ;
#7707=DIRECTION ( 'NONE',  ( -1.000000000000000000, 0.000000000000000000, 0.000000000000000000 ) ) ;
#7720=CARTESIAN_POINT ( 'NONE',  ( 7.795990775014339569, 74.32053629685827900, 3.000000000000002665 ) ) ;
#7730=CARTESIAN_POINT ( 'NONE',  ( 3.556430356250014579, 108.1539533981018053, 2.965625000614517504 ) ) ;
#7740=FACE_OUTER_BOUND ( 'NONE', #11068, .T. ) ;
#7743=CARTESIAN_POINT ( 'NONE',  ( 25.68387172342410807, 120.0032449382199928, 2.999999999999998224 ) ) ;
#7747=ORIENTED_EDGE ( 'NONE', *, *, #9329, .F. ) ;
#7748=CARTESIAN_POINT ( 'NONE',  ( 66.20000000000000284, 71.98667160128370313, 3.387500000000000178 ) ) ;
#7756=ADVANCED_FACE ( 'NONE', ( #9971 ), #1804, .T. ) ;
#7760=CARTESIAN_POINT ( 'NONE',  ( 66.44356964375000985, 71.84604660189820891, 4.596875000614516260 ) ) ;
#7761=ORIENTED_EDGE ( 'NONE', *, *, #10496, .F. ) ;
#7781=CARTESIAN_POINT ( 'NONE',  ( 11.55549086838933981, 69.15209071451751299, 3.000000000000000444 ) ) ;
#7786=VERTEX_POINT ( 'NONE', #6831 ) ;
#7788=ORIENTED_EDGE ( 'NONE', *, *, #300, .F. ) ;
#7790=CARTESIAN_POINT ( 'NONE',  ( 3.556430356250015024, 90.00000000000000000, 4.353125000614517681 ) ) ;
#7803=CLOSED_SHELL ( 'NONE', ( #7395, #3258, #11855, #3534, #5894, #7124, #9022, #6425, #8157, #7756, #10035, #7561, #11648, #482, #375, #4024, #10914, #11754, #11139, #2647, #12030, #9773, #7575 ) ) ;
#7805=ORIENTED_EDGE ( 'NONE', *, *, #5640, .F. ) ;
#7811=FACE_OUTER_BOUND ( 'NONE', #9215, .T. ) ;
#7827=ORIENTED_EDGE ( 'NONE', *, *, #10710, .T. ) ;
#7858=CARTESIAN_POINT ( 'NONE',  ( 50.72178482187501203, 62.76906990284730625, 3.153125000614517504 ) ) ;
#7879=ORIENTED_EDGE ( 'NONE', *, *, #831, .T. ) ;
#7880=CARTESIAN_POINT ( 'NONE',  ( 66.44356964374998142, 108.1539533981018053, 3.771875000614516971 ) ) ;
#7899=AXIS2_PLACEMENT_3D ( 'NONE', #9545, #8321, #7707 ) ;
#7902=DIRECTION ( 'NONE',  ( 0.000000000000000000, 0.000000000000000000, 1.000000000000000000 ) ) ;
#7915=EDGE_CURVE ( 'NONE', #7786, #998, #3114, .T. ) ;
#7937=CARTESIAN_POINT ( 'NONE',  ( 3.800000000000015365, 90.00000000000000000, 5.000000000000000000 ) ) ;
#7939=CIRCLE ( 'NONE', #6680, 32.70000000000000995 ) ;
#7946=CARTESIAN_POINT ( 'NONE',  ( 19.27821517812503060, 62.76906990284727783, 3.584375000614516971 ) ) ;
#7956=CARTESIAN_POINT ( 'NONE',  ( 19.27821517812500574, 117.2309300971526937, 4.784375000614516260 ) ) ;
#7976=ORIENTED_EDGE ( 'NONE', *, *, #1139, .F. ) ;
#7978=FACE_OUTER_BOUND ( 'NONE', #9567, .T. ) ;
#7990=CARTESIAN_POINT ( 'NONE',  ( 3.556430356250028790, 71.84604660189818048, 3.940625000614517592 ) ) ;
#7999=CARTESIAN_POINT ( 'NONE',  ( 64.29296370151269002, 100.7401778149417879, 3.000000000000000000 ) ) ;
#8001=CARTESIAN_POINT ( 'NONE',  ( 45.22164986280591847, 119.6006263581510183, 3.000000000000000444 ) ) ;
#8010=CARTESIAN_POINT ( 'NONE',  ( 50.72178482187499071, 117.2309300971526937, 3.359375000614517326 ) ) ;
#8020=CARTESIAN_POINT ( 'NONE',  ( 66.19999999999998863, 90.00000000000000000, 3.425000000000000266 ) ) ;
#8021=CARTESIAN_POINT ( 'NONE',  ( 50.72178482187499071, 117.2309300971526937, 3.359375000614517326 ) ) ;
#8025=AXIS2_PLACEMENT_3D ( 'NONE', #2873, #4954, #953 ) ;
#8036=CARTESIAN_POINT ( 'NONE',  ( 66.19999999999998863, 90.00000000000000000, 3.875000000000000000 ) ) ;
#8052=CARTESIAN_POINT ( 'NONE',  ( 35.00000000000000000, 126.3079067962035822, 3.340625000614517059 ) ) ;
#8055=CARTESIAN_POINT ( 'NONE',  ( 35.00000000000000711, 53.97334320256736362, 3.425000001229034474 ) ) ;
#8058=DIRECTION ( 'NONE',  ( 0.000000000000000000, 0.000000000000000000, -1.000000000000000000 ) ) ;
#8059=CARTESIAN_POINT ( 'NONE',  ( 66.44356964375000985, 71.84604660189820891, 4.540625000614517681 ) ) ;
#8060=CARTESIAN_POINT ( 'NONE',  ( 3.800000000000015365, 90.00000000000000000, 5.000000000000000000 ) ) ;
#8068=CARTESIAN_POINT ( 'NONE',  ( 63.34962933878586711, 103.3078946294862135, 3.000000000000001776 ) ) ;
#8077=CARTESIAN_POINT ( 'NONE',  ( 60.43447242791587826, 111.3420572944792895, 3.026359441279048657 ) ) ;
#8090=ORIENTED_EDGE ( 'NONE', *, *, #6990, .F. ) ;
#8107=( BOUNDED_SURFACE ( )  B_SPLINE_SURFACE ( 1, 2, ( 
 ( #9707, #11736, #12597, #2785, #804, #1798, #3900, #3706, #10754, #5784, #11806, #11613, #10570, #3768, #1606, #1670, #612, #12787, #5592, #744, #3641, #4869, #9775, #4744, #5720, #8730, #2659, #4808, #6633, #3831, #9585, #6764, #2853, #4618, #6825, #10819, #1864, #12726, #8858, #9838, #5656, #4680, #11543, #7748, #868, #12852, #8668, #2590, #11675, #2723, #6697, #10692, #1733, #8077, #6168 ),
 ( #5189, #9178, #8922, #7025, #3042, #11867, #6957, #2914, #11135, #11993, #2976, #7091, #3109, #9046, #10881, #4, #11072, #5907, #4026, #73, #2191, #201, #6894, #6038, #12062, #4937, #2124, #10091, #6100, #7880, #8981, #1127, #5121, #4152, #7946, #9113, #10161, #12916, #5055, #11006, #8010, #137, #1993, #3962, #8143, #11932, #5973, #12129, #10943, #9968, #4088, #3175, #1926, #999, #7152 ) ),
 .UNSPECIFIED., .F., .F., .F. ) 
 B_SPLINE_SURFACE_WITH_KNOTS ( ( 2, 2 ),
 ( 3, 2, 2, 2, 2, 2, 2, 2, 2, 2, 2, 2, 2, 2, 2, 2, 2, 2, 2, 2, 2, 2, 2, 2, 2, 2, 2, 3 ),
 ( 0.000000000000000000, 1.000000000000000000 ),
 ( 0.000000000000000000, 0.03333333333333333287, 0.06666666666666666574, 0.1000000000000000056, 0.1333333333333333315, 0.1666666666666666574, 0.2000000000000000111, 0.2333333333333333370, 0.2666666666666666630, 0.2999999999999999889, 0.3333333333333333148, 0.3666666666666666408, 0.4000000000000000222, 0.4333333333333333481, 0.4666666666666666741, 0.5000000000000000000, 0.5333333333333333259, 0.5666666666666666519, 0.5999999999999999778, 0.6333333333333333037, 0.6666666666666666297, 0.6999999999999999556, 0.7333333333333332815, 0.7666666666666667185, 0.8000000000000000444, 0.8333333333333333703, 0.8666666666666666963, 0.8887752010443024098 ),
 .UNSPECIFIED. ) 
 GEOMETRIC_REPRESENTATION_ITEM ( )  RATIONAL_B_SPLINE_SURFACE ( (
 ( 1.000000000000000000, 0.8660254037844387076, 1.000000000000000000, 0.8660254037844387076, 1.000000000000000000, 0.8660254037844387076, 1.000000000000000000, 0.8660254037844387076, 1.000000000000000000, 0.8660254037844387076, 1.000000000000000000, 0.8660254037844387076, 1.000000000000000000, 0.8660254037844387076, 1.000000000000000000, 0.8660254037844387076, 1.000000000000000000, 0.8660254037844387076, 1.000000000000000000, 0.8660254037844387076, 1.000000000000000000, 0.8660254037844387076, 1.000000000000000000, 0.8660254037844387076, 1.000000000000000000, 0.8660254037844387076, 1.000000000000000000, 0.8660254037844387076, 1.000000000000000000, 0.8660254037844387076, 1.000000000000000000, 0.8660254037844387076, 1.000000000000000000, 0.8660254037844387076, 1.000000000000000000, 0.8660254037844387076, 1.000000000000000000, 0.8660254037844387076, 1.000000000000000000, 0.8660254037844387076, 1.000000000000000000, 0.8660254037844387076, 1.000000000000000000, 0.8660254037844387076, 1.000000000000000000, 0.8660254037844387076, 1.000000000000000000, 0.8660254037844387076, 1.000000000000000000, 0.8660254037844387076, 1.000000000000000000, 0.8660254037844387076, 1.000000000000000000, 0.9111405410151519613, 0.9401542262549813511),
 ( 1.000000000000000000, 0.8660254037844387076, 1.000000000000000000, 0.8660254037844387076, 1.000000000000000000, 0.8660254037844387076, 1.000000000000000000, 0.8660254037844387076, 1.000000000000000000, 0.8660254037844387076, 1.000000000000000000, 0.8660254037844387076, 1.000000000000000000, 0.8660254037844387076, 1.000000000000000000, 0.8660254037844387076, 1.000000000000000000, 0.8660254037844387076, 1.000000000000000000, 0.8660254037844387076, 1.000000000000000000, 0.8660254037844387076, 1.000000000000000000, 0.8660254037844387076, 1.000000000000000000, 0.8660254037844387076, 1.000000000000000000, 0.8660254037844387076, 1.000000000000000000, 0.8660254037844387076, 1.000000000000000000, 0.8660254037844387076, 1.000000000000000000, 0.8660254037844387076, 1.000000000000000000, 0.8660254037844387076, 1.000000000000000000, 0.8660254037844387076, 1.000000000000000000, 0.8660254037844387076, 1.000000000000000000, 0.8660254037844387076, 1.000000000000000000, 0.8660254037844387076, 1.000000000000000000, 0.8660254037844387076, 1.000000000000000000, 0.8660254037844387076, 1.000000000000000000, 0.8660254037844387076, 1.000000000000000000, 0.8660254037844387076, 1.000000000000000000, 0.9111405410151519613, 0.9401542262549813511) ) ) 
 REPRESENTATION_ITEM ( '' )  SURFACE ( )  );
#8116=CARTESIAN_POINT ( 'NONE',  ( 64.54728994471078352, 100.7543353520590870, 2.802601390178781404 ) ) ;
#8141=EDGE_CURVE ( 'NONE', #4442, #3844, #6760, .T. ) ;
#8143=CARTESIAN_POINT ( 'NONE',  ( 50.72178482187501203, 62.76906990284730625, 3.209375000614517415 ) ) ;
#8152=CARTESIAN_POINT ( 'NONE',  ( 66.44356964374998142, 108.1539533981018053, 3.321875000614517237 ) ) ;
#8157=ADVANCED_FACE ( 'NONE', ( #7740 ), #1723, .F. ) ;
#8166=CARTESIAN_POINT ( 'NONE',  ( 35.00000000000000000, 90.00000000000000000, 3.000000000000000000 ) ) ;
#8173=DIRECTION ( 'NONE',  ( -0.000000000000000000, -0.000000000000000000, -1.000000000000000000 ) ) ;
#8178=CARTESIAN_POINT ( 'NONE',  ( 35.00000000000000711, 53.69209320379640360, 4.465625000614517504 ) ) ;
#8180=VECTOR ( 'NONE', #8058, 1000.000000000000000 ) ;
#8187=CARTESIAN_POINT ( 'NONE',  ( 19.27821517812503060, 62.76906990284727783, 4.428125000614516971 ) ) ;
#8215=CARTESIAN_POINT ( 'NONE',  ( 66.44356964374998142, 108.1539533981018053, 3.771875000614516082 ) ) ;
#8224=MECHANICAL_DESIGN_GEOMETRIC_PRESENTATION_REPRESENTATION('',(#11566),#7391);
#8246=CARTESIAN_POINT ( 'NONE',  ( 66.44356964374998142, 108.1539533981018053, 3.265625000614516882 ) ) ;
#8263=CARTESIAN_POINT ( 'NONE',  ( 3.800000000000135270, 108.0133283987163679, 3.162500000000000533 ) ) ;
#8312=CARTESIAN_POINT ( 'NONE',  ( 50.72178482187499071, 117.2309300971526937, 4.203125000614517326 ) ) ;
#8314=ORIENTED_EDGE ( 'NONE', *, *, #831, .F. ) ;
#8321=DIRECTION ( 'NONE',  ( -0.000000000000000000, -0.000000000000000000, -1.000000000000000000 ) ) ;
#8326=EDGE_CURVE ( 'NONE', #11494, #12628, #925, .T. ) ;
#8339=( BOUNDED_CURVE ( )  B_SPLINE_CURVE ( 2, ( #10153, #8263, #12252, #5309, #9104, #3299, #11324 ),
 .UNSPECIFIED., .F., .F. ) 
 B_SPLINE_CURVE_WITH_KNOTS ( ( 3, 2, 2, 3 ),
 ( 0.8000000000000002665, 0.8333333333333334814, 0.8666666666666666963, 0.8885532418875740079 ),
 .UNSPECIFIED. ) 
 CURVE ( )  GEOMETRIC_REPRESENTATION_ITEM ( )  RATIONAL_B_SPLINE_CURVE ( ( 0.9999999999999991118, 0.8660254037844395958, 1.000000000000000000, 0.8660254037844387076, 1.000000000000000000, 0.9120326476671229976, 0.9395835397633002239 ) ) 
 REPRESENTATION_ITEM ( '' )  );
#8346=DIRECTION ( 'NONE',  ( -0.000000000000000000, -0.000000000000000000, -1.000000000000000000 ) ) ;
#8354=CARTESIAN_POINT ( 'NONE',  ( 66.19999999999998863, 90.00000000000000000, 4.437500001229033764 ) ) ;
#8356=CARTESIAN_POINT ( 'NONE',  ( 66.20000000000000284, 90.00000000000000000, 6.000000000000000000 ) ) ;
#8379=CARTESIAN_POINT ( 'NONE',  ( 66.20000000000000284, 71.98667160128370313, 3.050000001229034474 ) ) ;
#8388=SURFACE_STYLE_FILL_AREA ( #10410 ) ;
#8389=ORIENTED_EDGE ( 'NONE', *, *, #12796, .F. ) ;
#8394=CARTESIAN_POINT ( 'NONE',  ( 66.44356964374999563, 71.84604660189820891, 3.246875000614517059 ) ) ;
#8397=DIRECTION ( 'NONE',  ( 0.000000000000000000, 1.000000000000000000, 0.000000000000000000 ) ) ;
#8398=CARTESIAN_POINT ( 'NONE',  ( 35.00000000000000000, 90.00000000000000000, 3.000000000000000000 ) ) ;
#8403=CARTESIAN_POINT ( 'NONE',  ( 33.50000000000000711, 67.79999999999999716, 8.000000000000000000 ) ) ;
#8419=CARTESIAN_POINT ( 'NONE',  ( 66.19999999999998863, 90.00000000000000000, 3.087500001229034119 ) ) ;
#8430=CARTESIAN_POINT ( 'NONE',  ( 3.800000000000055334, 71.98667160128364628, 3.800000001229034474 ) ) ;
#8440=CARTESIAN_POINT ( 'NONE',  ( 50.59999999999999432, 117.0199925980744666, 2.712500001229034119 ) ) ;
#8443=ORIENTED_EDGE ( 'NONE', *, *, #4228, .T. ) ;
#8455=CARTESIAN_POINT ( 'NONE',  ( 3.800000000000015365, 90.00000000000000000, 3.312500001229034652 ) ) ;
#8458=CARTESIAN_POINT ( 'NONE',  ( 3.556430356250015024, 90.00000000000000000, 3.059375000614517059 ) ) ;
#8460=ORIENTED_EDGE ( 'NONE', *, *, #3785, .F. ) ;
#8467=CYLINDRICAL_SURFACE ( 'NONE', #379, 31.19999999999999929 ) ;
#8469=CARTESIAN_POINT ( 'NONE',  ( 3.800000000000015365, 90.00000000000000000, 3.650000000000000355 ) ) ;
#8483=EDGE_CURVE ( 'NONE', #10249, #10977, #3012, .T. ) ;
#8485=CARTESIAN_POINT ( 'NONE',  ( 3.800000000000039790, 71.98667160128364628, 4.587500000000000355 ) ) ;
#8493=ORIENTED_EDGE ( 'NONE', *, *, #4395, .F. ) ;
#8497=LINE ( 'NONE', #6454, #1824 ) ;
#8505=ORIENTED_EDGE ( 'NONE', *, *, #11585, .F. ) ;
#8506=DIRECTION ( 'NONE',  ( -0.000000000000000000, -0.000000000000000000, -1.000000000000000000 ) ) ;
#8507=CARTESIAN_POINT ( 'NONE',  ( 35.00000000000000711, 53.97334320256736362, 3.875000001229034208 ) ) ;
#8515=CARTESIAN_POINT ( 'NONE',  ( 20.04920293992519831, 62.48814478912512982, 3.000000000000001776 ) ) ;
#8529=CARTESIAN_POINT ( 'NONE',  ( 10.10814115972632088, 109.2382489648782240, 3.000000000000001332 ) ) ;
#8533=APPLICATION_CONTEXT ( 'automotive_design' ) ;
#8545=VERTEX_POINT ( 'NONE', #2232 ) ;
#8576=CARTESIAN_POINT ( 'NONE',  ( 3.800000000000015365, 108.0133283987163111, 4.175000001229034474 ) ) ;
#8580=CARTESIAN_POINT ( 'NONE',  ( 10.32967766089132233, 70.63732739706711072, 3.000000000000001776 ) ) ;
#8591=CARTESIAN_POINT ( 'NONE',  ( 66.44356964374998142, 108.1539533981018053, 4.221875000614517148 ) ) ;
#8594=CARTESIAN_POINT ( 'NONE',  ( 12.79502542898369555, 112.2861453170762474, 2.999999999999998224 ) ) ;
#8597=AXIS2_PLACEMENT_3D ( 'NONE', #1730, #4740, #10751 ) ;
#8606=CARTESIAN_POINT ( 'NONE',  ( 3.800000000000015365, 90.00000000000000000, 3.650000000000000355 ) ) ;
#8622=CARTESIAN_POINT ( 'NONE',  ( 3.800000000000015365, 90.00000000000000000, 4.549999999999999822 ) ) ;
#8634=CARTESIAN_POINT ( 'NONE',  ( 66.19999999999998863, 90.00000000000000000, 3.087500001229034119 ) ) ;
#8651=CARTESIAN_POINT ( 'NONE',  ( 66.44356964374999563, 71.84604660189820891, 4.596875000614517148 ) ) ;
#8668=CARTESIAN_POINT ( 'NONE',  ( 19.40000000000002700, 62.98000740192551206, 3.275000000000000355 ) ) ;
#8676=DIRECTION ( 'NONE',  ( 0.000000000000000000, 0.000000000000000000, 1.000000000000000000 ) ) ;
#8685=CARTESIAN_POINT ( 'NONE',  ( 35.00000000000000000, 126.0266567974326222, 4.437500000000000888 ) ) ;
#8688=CARTESIAN_POINT ( 'NONE',  ( 33.50000000000000711, 67.79999999999999716, 6.000000000000000000 ) ) ;
#8699=CARTESIAN_POINT ( 'NONE',  ( 35.00000000000000000, 90.00000000000000000, 6.000000000000000000 ) ) ;
#8703=CARTESIAN_POINT ( 'NONE',  ( 7.180262550876764571, 75.42990296268297357, 3.000000000000000444 ) ) ;
#8705=ORIENTED_EDGE ( 'NONE', *, *, #8483, .T. ) ;
#8711=EDGE_LOOP ( 'NONE', ( #2641, #4179, #5703, #1168 ) ) ;
#8712=CARTESIAN_POINT ( 'NONE',  ( 50.72178482187499071, 117.2309300971526937, 2.853125000614517237 ) ) ;
#8713=ORIENTED_EDGE ( 'NONE', *, *, #4432, .F. ) ;
#8715=CARTESIAN_POINT ( 'NONE',  ( 66.20000000000004547, 108.0133283987162969, 3.912500000000000977 ) ) ;
#8730=CARTESIAN_POINT ( 'NONE',  ( 3.800000000000015365, 108.0133283987163111, 4.062500000000000000 ) ) ;
#8742=CARTESIAN_POINT ( 'NONE',  ( 50.72178482187499071, 117.2309300971526937, 4.259375000614517681 ) ) ;
#8746=DIRECTION ( 'NONE',  ( -1.000000000000000000, -0.000000000000000000, -0.000000000000000000 ) ) ;
#8751=EDGE_CURVE ( 'NONE', #12799, #9156, #4499, .T. ) ;
#8766=CARTESIAN_POINT ( 'NONE',  ( 42.94697885295607165, 59.81164240722340963, 2.999999999999999112 ) ) ;
#8776=CARTESIAN_POINT ( 'NONE',  ( 19.27821517812503060, 62.76906990284727783, 3.978125000614516793 ) ) ;
#8784=CARTESIAN_POINT ( 'NONE',  ( 19.40000000000002700, 62.98000740192551206, 4.287500001229034297 ) ) ;
#8791=DIRECTION ( 'NONE',  ( -1.000000000000000000, 0.000000000000000000, 0.000000000000000000 ) ) ;
#8805=CARTESIAN_POINT ( 'NONE',  ( 35.00000000000000000, 126.3079067962036106, 3.846875000614517592 ) ) ;
#8819=ORIENTED_EDGE ( 'NONE', *, *, #1171, .F. ) ;
#8834=CARTESIAN_POINT ( 'NONE',  ( 35.00000000000000711, 53.69209320379640360, 3.565625000614517592 ) ) ;
#8840=CARTESIAN_POINT ( 'NONE',  ( 66.19999999999998863, 90.00000000000000000, 4.774999999999999467 ) ) ;
#8858=CARTESIAN_POINT ( 'NONE',  ( 19.40000000000000924, 117.0199925980744666, 3.575000000000000178 ) ) ;
#8890=ORIENTED_EDGE ( 'NONE', *, *, #7379, .T. ) ;
#8920=FACE_OUTER_BOUND ( 'NONE', #4840, .T. ) ;
#8922=CARTESIAN_POINT ( 'NONE',  ( 19.27821517812500574, 117.2309300971526937, 4.784375000614516260 ) ) ;
#8936=CARTESIAN_POINT ( 'NONE',  ( 2.300000000000003375, 90.00000000000000000, 6.000000000000000000 ) ) ;
#8961=CARTESIAN_POINT ( 'NONE',  ( 66.44356964374998142, 108.1539533981018053, 4.165625000614516793 ) ) ;
#8974=CARTESIAN_POINT ( 'NONE',  ( 3.800000000000004707, 90.00000000000000000, 6.000000000000000000 ) ) ;
#8977=VERTEX_POINT ( 'NONE', #340 ) ;
#8981=CARTESIAN_POINT ( 'NONE',  ( 66.44356964374999563, 90.00000000000000000, 3.734375000614516882 ) ) ;
#8997=CARTESIAN_POINT ( 'NONE',  ( 0.000000000000000000, 0.000000000000000000, 0.000000000000000000 ) ) ;
#9022=ADVANCED_FACE ( 'NONE', ( #10166 ), #9184, .F. ) ;
#9023=CARTESIAN_POINT ( 'NONE',  ( 50.72178482187499071, 117.2309300971526937, 3.303125000614517415 ) ) ;
#9029=CARTESIAN_POINT ( 'NONE',  ( 66.44356964375000985, 71.84604660189820891, 3.190625000614517592 ) ) ;
#9032=EDGE_CURVE ( 'NONE', #5860, #11494, #6242, .T. ) ;
#9037=DIRECTION ( 'NONE',  ( -0.000000000000000000, -0.000000000000000000, -1.000000000000000000 ) ) ;
#9046=CARTESIAN_POINT ( 'NONE',  ( 3.556430356250014579, 108.1539533981018053, 4.371875000614517504 ) ) ;
#9064=EDGE_CURVE ( 'NONE', #10795, #10977, #1940, .T. ) ;
#9079=CARTESIAN_POINT ( 'NONE',  ( 67.70000000000001705, 90.00000000000000000, 8.000000000000000000 ) ) ;
#9082=AXIS2_PLACEMENT_3D ( 'NONE', #5760, #10856, #12822 ) ;
#9087=CARTESIAN_POINT ( 'NONE',  ( 66.44356964374999563, 90.00000000000000000, 4.578125000614516438 ) ) ;
#9104=CARTESIAN_POINT ( 'NONE',  ( 50.59999999999999432, 117.0199925980744666, 3.050000000000000266 ) ) ;
#9113=CARTESIAN_POINT ( 'NONE',  ( 3.556430356250028790, 71.84604660189818048, 3.546875000614516882 ) ) ;
#9132=LINE ( 'NONE', #8356, #5919 ) ;
#9152=CARTESIAN_POINT ( 'NONE',  ( 66.44356964374999563, 90.00000000000000000, 4.128125000614517148 ) ) ;
#9156=VERTEX_POINT ( 'NONE', #12459 ) ;
#9158=CARTESIAN_POINT ( 'NONE',  ( 35.00000000000000000, 126.3079067962036106, 4.690625000614517148 ) ) ;
#9165=VERTEX_POINT ( 'NONE', #1526 ) ;
#9174=UNCERTAINTY_MEASURE_WITH_UNIT (LENGTH_MEASURE( 1.000000000000000082E-05 ), #9424, 'distance_accuracy_value', 'NONE');
#9178=CARTESIAN_POINT ( 'NONE',  ( 3.556430356250014579, 108.1539533981018053, 4.821875000614516793 ) ) ;
#9184=CYLINDRICAL_SURFACE ( 'NONE', #1867, 31.19999999999999929 ) ;
#9198=CARTESIAN_POINT ( 'NONE',  ( 35.00000000000000000, 126.0266567974326222, 4.100000001229034297 ) ) ;
#9215=EDGE_LOOP ( 'NONE', ( #11259, #7747, #7805, #6956, #12419, #6472, #8090, #8493, #2226, #6321, #2057, #4657 ) ) ;
#9217=CARTESIAN_POINT ( 'NONE',  ( 66.44356964374998142, 108.1539533981018053, 3.715625000614517948 ) ) ;
#9218=ORIENTED_EDGE ( 'NONE', *, *, #9788, .T. ) ;
#9225=CARTESIAN_POINT ( 'NONE',  ( 35.00000000000000711, 53.69209320379639649, 4.465625000614517504 ) ) ;
#9247=( BOUNDED_CURVE ( )  B_SPLINE_CURVE ( 2, ( #7013, #7139, #124, #11057, #3227, #4075, #10993 ),
 .UNSPECIFIED., .F., .F. ) 
 B_SPLINE_CURVE_WITH_KNOTS ( ( 3, 2, 2, 3 ),
 ( 0.3000000000000002109, 0.3333333333333334259, 0.3666666666666666963, 0.3999999999999999667 ),
 .UNSPECIFIED. ) 
 CURVE ( )  GEOMETRIC_REPRESENTATION_ITEM ( )  RATIONAL_B_SPLINE_CURVE ( ( 0.9999999999999991118, 0.8660254037844395958, 1.000000000000000000, 0.8660254037844387076, 1.000000000000000000, 0.8660254037844389297, 0.9999999999999997780 ) ) 
 REPRESENTATION_ITEM ( '' )  );
#9253=DIRECTION ( 'NONE',  ( 0.000000000000000000, 0.000000000000000000, 1.000000000000000000 ) ) ;
#9269=CARTESIAN_POINT ( 'NONE',  ( 35.00000000000000000, 90.00000000000000000, 8.000000000000000000 ) ) ;
#9283=PRODUCT_DEFINITION_SHAPE ( 'NONE', 'NONE',  #10255 ) ;
#9287=VERTEX_POINT ( 'NONE', #3759 ) ;
#9288=CARTESIAN_POINT ( 'NONE',  ( 3.800000000000015365, 108.0133283987163111, 4.625000001229034652 ) ) ;
#9297=CYLINDRICAL_SURFACE ( 'NONE', #7899, 31.19999999999999929 ) ;
#9323=CARTESIAN_POINT ( 'NONE',  ( 36.50000000000001421, 79.80000000000001137, 8.000000000000000000 ) ) ;
#9324=CARTESIAN_POINT ( 'NONE',  ( 64.24207199149496716, 100.8784753363798075, 2.999999999999999556 ) ) ;
#9329=EDGE_CURVE ( 'NONE', #4968, #3844, #8339, .T. ) ;
#9335=DIRECTION ( 'NONE',  ( 0.000000000000000000, 0.000000000000000000, 1.000000000000000000 ) ) ;
#9350=CARTESIAN_POINT ( 'NONE',  ( 37.73448666702899601, 121.2272378967086013, 3.000000000000000888 ) ) ;
#9352=CARTESIAN_POINT ( 'NONE',  ( 66.19999999999998863, 90.00000000000000000, 3.537500001229034297 ) ) ;
#9356=ORIENTED_EDGE ( 'NONE', *, *, #1139, .T. ) ;
#9358=FACE_OUTER_BOUND ( 'NONE', #10930, .T. ) ;
#9368=CARTESIAN_POINT ( 'NONE',  ( 3.556430356250028790, 71.84604660189818048, 3.996875000614517059 ) ) ;
#9369=ORIENTED_EDGE ( 'NONE', *, *, #11585, .T. ) ;
#9385=CARTESIAN_POINT ( 'NONE',  ( 3.799999999999985612, 108.0133283987162827, 3.725000001229034741 ) ) ;
#9397=DIRECTION ( 'NONE',  ( 1.000000000000000000, 0.000000000000000000, 0.000000000000000000 ) ) ;
#9406=ORIENTED_EDGE ( 'NONE', *, *, #7915, .T. ) ;
#9412=CARTESIAN_POINT ( 'NONE',  ( 31.93836427709092973, 121.3209901524069636, 3.000000000000000444 ) ) ;
#9424=( LENGTH_UNIT ( ) NAMED_UNIT ( * ) SI_UNIT ( .MILLI., .METRE. ) );
#9431=CARTESIAN_POINT ( 'NONE',  ( 3.556430356250014579, 108.1539533981018053, 3.021875000614517415 ) ) ;
#9480=CARTESIAN_POINT ( 'NONE',  ( 66.19999999999998863, 90.00000000000000000, 4.437500001229033764 ) ) ;
#9485=LINE ( 'NONE', #3544, #4004 ) ;
#9494=CARTESIAN_POINT ( 'NONE',  ( 19.27821517812500574, 117.2309300971526937, 4.728125000614516793 ) ) ;
#9500=CARTESIAN_POINT ( 'NONE',  ( 19.27821517812500574, 117.2309300971526937, 4.784375000614516260 ) ) ;
#9504=CARTESIAN_POINT ( 'NONE',  ( 4.995430082848484332, 99.45808535391196870, 2.999999999999999112 ) ) ;
#9545=CARTESIAN_POINT ( 'NONE',  ( 35.00000000000000000, 90.00000000000000000, 6.000000000000000000 ) ) ;
#9546=ORIENTED_EDGE ( 'NONE', *, *, #3194, .T. ) ;
#9555=FACE_OUTER_BOUND ( 'NONE', #3913, .T. ) ;
#9557=CARTESIAN_POINT ( 'NONE',  ( 15.79116220520106495, 65.24871774101997346, 3.000000000000002220 ) ) ;
#9564=CARTESIAN_POINT ( 'NONE',  ( 66.19999999999998863, 90.00000000000000000, 3.087500001229034119 ) ) ;
#9566=CARTESIAN_POINT ( 'NONE',  ( 19.27821517812500574, 117.2309300971526937, 3.884375000614516793 ) ) ;
#9567=EDGE_LOOP ( 'NONE', ( #687, #6356, #10569 ) ) ;
#9573=DIRECTION ( 'NONE',  ( -0.000000000000000000, -0.000000000000000000, -1.000000000000000000 ) ) ;
#9574=DIRECTION ( 'NONE',  ( 1.000000000000000000, 0.000000000000000000, 0.000000000000000000 ) ) ;
#9583=EDGE_CURVE ( 'NONE', #5750, #9165, #295, .T. ) ;
#9585=CARTESIAN_POINT ( 'NONE',  ( 66.19999999999998863, 90.00000000000000000, 3.875000000000000000 ) ) ;
#9613=CARTESIAN_POINT ( 'NONE',  ( 19.40000000000000924, 117.0199925980744666, 2.787500001229034297 ) ) ;
#9620=CARTESIAN_POINT ( 'NONE',  ( 39.18799846562198042, 59.03019923891626064, 3.000000000000000000 ) ) ;
#9629=ORIENTED_EDGE ( 'NONE', *, *, #6990, .T. ) ;
#9630=CARTESIAN_POINT ( 'NONE',  ( 66.44356964374998142, 108.1539533981018053, 4.671875000614516438 ) ) ;
#9632=EDGE_LOOP ( 'NONE', ( #11558, #2342, #5522, #5249 ) ) ;
#9653=CARTESIAN_POINT ( 'NONE',  ( 35.00000000000000000, 90.00000000000000000, 8.000000000000000000 ) ) ;
#9667=ORIENTED_EDGE ( 'NONE', *, *, #1409, .T. ) ;
#9671=B_SPLINE_CURVE_WITH_KNOTS ( 'NONE', 3,
 ( #3679, #5629, #10470, #8766, #6731, #2561, #9620, #1705, #582, #5491, #4524, #12634, #3612, #6539, #1506, #2499, #8515, #11580, #3802, #9557, #648, #4587, #11645, #6669, #7781, #8580, #2757, #4717, #12573, #7720, #8703, #7591, #11708, #2629, #6604, #7531, #10723, #4779, #1640, #10537 ),
 .UNSPECIFIED., .F., .F.,
 ( 4, 2, 2, 2, 2, 2, 2, 2, 2, 2, 2, 2, 2, 2, 2, 2, 2, 2, 2, 4 ),
 ( 0.000000000000000000, 0.001930134362530089298, 0.003860268725060178596, 0.007720537450120362397, 0.01158080617518054620, 0.01544107490024072826, 0.02316161235036109586, 0.02509174671289119210, 0.02702188107542128834, 0.03088214980048148428, 0.03281228416301156664, 0.03474241852554164900, 0.03860268725060180678, 0.04053282161313188914, 0.04246295597566197150, 0.04632322470072212928, 0.05018349342578230093, 0.05404376215084246565, 0.05790403087590263037, 0.06176429960096278815 ),
 .UNSPECIFIED. ) ;
#9689=CARTESIAN_POINT ( 'NONE',  ( 3.556430356250015024, 90.00000000000000000, 3.903125000614517504 ) ) ;
#9702=CARTESIAN_POINT ( 'NONE',  ( 22.06359219780243208, 118.6456930160215251, 2.999999999999998668 ) ) ;
#9707=CARTESIAN_POINT ( 'NONE',  ( 3.800000000000015365, 90.00000000000000000, 5.000000000000000000 ) ) ;
#9727=CARTESIAN_POINT ( 'NONE',  ( 66.19999999999998863, 90.00000000000000000, 3.987500001229034030 ) ) ;
#9757=CARTESIAN_POINT ( 'NONE',  ( 3.556430356250028790, 71.84604660189818048, 4.390625000614517326 ) ) ;
#9773=ADVANCED_FACE ( 'NONE', ( #5763 ), #10083, .T. ) ;
#9775=CARTESIAN_POINT ( 'NONE',  ( 19.40000000000002700, 62.98000740192551206, 4.174999999999999822 ) ) ;
#9777=EDGE_LOOP ( 'NONE', ( #5533, #11092, #9667, #8705 ) ) ;
#9787=CARTESIAN_POINT ( 'NONE',  ( 35.00000000000000000, 126.3079067962036106, 4.746875000614517504 ) ) ;
#9788=EDGE_CURVE ( 'NONE', #11574, #7460, #6836, .T. ) ;
#9803=ORIENTED_EDGE ( 'NONE', *, *, #1171, .T. ) ;
#9819=CARTESIAN_POINT ( 'NONE',  ( 35.00000000000000711, 53.69209320379640360, 3.115625000614517415 ) ) ;
#9828=CARTESIAN_POINT ( 'NONE',  ( 50.60000000000001563, 62.98000740192552627, 4.700000000000000178 ) ) ;
#9838=CARTESIAN_POINT ( 'NONE',  ( 35.00000000000000000, 126.0266567974326222, 3.537500000000000089 ) ) ;
#9849=CARTESIAN_POINT ( 'NONE',  ( 19.27821517812503060, 62.76906990284727783, 4.484375000614516438 ) ) ;
#9878=CARTESIAN_POINT ( 'NONE',  ( 50.72178482187501203, 62.76906990284730625, 3.603125000614517681 ) ) ;
#9888=ORIENTED_EDGE ( 'NONE', *, *, #188, .F. ) ;
#9891=CARTESIAN_POINT ( 'NONE',  ( 15.50185732988873077, 114.6638150138266639, 2.999999999999999112 ) ) ;
#9921=VECTOR ( 'NONE', #2031, 1000.000000000000000 ) ;
#9922=ORIENTED_EDGE ( 'NONE', *, *, #12440, .F. ) ;
#9931=FACE_OUTER_BOUND ( 'NONE', #1925, .T. ) ;
#9947=CARTESIAN_POINT ( 'NONE',  ( 35.00000000000000000, 126.3079067962035822, 4.240625000614517859 ) ) ;
#9952=CARTESIAN_POINT ( 'NONE',  ( 66.20000000000005969, 108.0133283987162685, 4.812499999999999112 ) ) ;
#9968=CARTESIAN_POINT ( 'NONE',  ( 3.556430356250014579, 108.1539533981018053, 3.021875000614517415 ) ) ;
#9971=FACE_OUTER_BOUND ( 'NONE', #6983, .T. ) ;
#9981=CARTESIAN_POINT ( 'NONE',  ( 33.50000000000000711, 79.80000000000001137, 6.000000000000000000 ) ) ;
#10007=CARTESIAN_POINT ( 'NONE',  ( 3.556430356250028790, 71.84604660189818048, 3.490625000614517415 ) ) ;
#10010=CARTESIAN_POINT ( 'NONE',  ( 3.800000000000025580, 71.98667160128366049, 3.350000001229034297 ) ) ;
#10012=( BOUNDED_CURVE ( )  B_SPLINE_CURVE ( 2, ( #8060, #12901, #3158, #6019, #52, #9952, #8840 ),
 .UNSPECIFIED., .F., .F. ) 
 B_SPLINE_CURVE_WITH_KNOTS ( ( 3, 2, 2, 3 ),
 ( 0.000000000000000000, 0.03333333333333339532, 0.06666666666666679064, 0.1000000000000001860 ),
 .UNSPECIFIED. ) 
 CURVE ( )  GEOMETRIC_REPRESENTATION_ITEM ( )  RATIONAL_B_SPLINE_CURVE ( ( 1.000000000000000000, 0.8660254037844387076, 1.000000000000000000, 0.8660254037844387076, 1.000000000000000000, 0.8660254037844380415, 1.000000000000000666 ) ) 
 REPRESENTATION_ITEM ( '' )  );
#10014=CARTESIAN_POINT ( 'NONE',  ( 3.556430356250015024, 90.00000000000000000, 4.353125000614517681 ) ) ;
#10023=CARTESIAN_POINT ( 'NONE',  ( 62.18023010225326175, 105.5722019109657310, 2.999999999999999556 ) ) ;
#10035=ADVANCED_FACE ( 'NONE', ( #3133, #5277 ), #2284, .F. ) ;
#10037=EDGE_CURVE ( 'NONE', #451, #6711, #11228, .T. ) ;
#10042=CARTESIAN_POINT ( 'NONE',  ( 66.44356964374999563, 90.00000000000000000, 3.284375000614517148 ) ) ;
#10052=CARTESIAN_POINT ( 'NONE',  ( 3.800000000000025580, 71.98667160128366049, 3.687500000000000888 ) ) ;
#10066=CARTESIAN_POINT ( 'NONE',  ( 3.556430356250014579, 108.1539533981018053, 2.965625000614517504 ) ) ;
#10083=( BOUNDED_SURFACE ( )  B_SPLINE_SURFACE ( 1, 2, ( 
 ( #4784, #4321, #2301, #11045, #5163, #10202, #9087, #1038, #44, #8178, #12099, #2100, #6010, #10981, #4061, #7129, #8312, #5095, #9152, #114, #311, #6211, #2235, #5230, #10132, #7063, #12038, #1238, #176, #9217, #12298, #3284, #241, #7194, #11246, #10007, #1302, #5033, #4129, #8052, #9023, #8246, #6078, #3085, #4259, #7261, #2162, #6276, #3349, #10066, #1102, #12235, #10265, #5294, #8116 ),
 ( #3149, #9288, #11111, #4193, #6137, #2033, #1170, #12168, #3216, #11180, #11374, #10529, #2427, #8576, #5356, #11506, #11573, #374, #3604, #1566, #2620, #8507, #641, #1633, #6402, #439, #5554, #7524, #12363, #3410, #9352, #11309, #10597, #2554, #12627, #6533, #6597, #6468, #5621, #7325, #10400, #4645, #8634, #8379, #10464, #2492, #2360, #7585, #1432, #5420, #9613, #6335, #8440, #12564, #10335 ) ),
 .UNSPECIFIED., .F., .F., .F. ) 
 B_SPLINE_SURFACE_WITH_KNOTS ( ( 2, 2 ),
 ( 3, 2, 2, 2, 2, 2, 2, 2, 2, 2, 2, 2, 2, 2, 2, 2, 2, 2, 2, 2, 2, 2, 2, 2, 2, 2, 2, 3 ),
 ( 0.000000000000000000, 1.000000000000000000 ),
 ( 0.000000000000000000, 0.03333333333333333287, 0.06666666666666666574, 0.1000000000000000056, 0.1333333333333333315, 0.1666666666666666574, 0.2000000000000000111, 0.2333333333333333370, 0.2666666666666666630, 0.2999999999999999889, 0.3333333333333333148, 0.3666666666666666408, 0.4000000000000000222, 0.4333333333333333481, 0.4666666666666666741, 0.5000000000000000000, 0.5333333333333333259, 0.5666666666666666519, 0.5999999999999999778, 0.6333333333333333037, 0.6666666666666666297, 0.6999999999999999556, 0.7333333333333332815, 0.7666666666666667185, 0.8000000000000000444, 0.8333333333333333703, 0.8666666666666666963, 0.8887752010635167066 ),
 .UNSPECIFIED. ) 
 GEOMETRIC_REPRESENTATION_ITEM ( )  RATIONAL_B_SPLINE_SURFACE ( (
 ( 1.000000000000000000, 0.8660254037844387076, 1.000000000000000000, 0.8660254037844387076, 1.000000000000000000, 0.8660254037844387076, 1.000000000000000000, 0.8660254037844387076, 1.000000000000000000, 0.8660254037844387076, 1.000000000000000000, 0.8660254037844387076, 1.000000000000000000, 0.8660254037844387076, 1.000000000000000000, 0.8660254037844387076, 1.000000000000000000, 0.8660254037844387076, 1.000000000000000000, 0.8660254037844387076, 1.000000000000000000, 0.8660254037844387076, 1.000000000000000000, 0.8660254037844387076, 1.000000000000000000, 0.8660254037844387076, 1.000000000000000000, 0.8660254037844387076, 1.000000000000000000, 0.8660254037844387076, 1.000000000000000000, 0.8660254037844387076, 1.000000000000000000, 0.8660254037844387076, 1.000000000000000000, 0.8660254037844387076, 1.000000000000000000, 0.8660254037844387076, 1.000000000000000000, 0.8660254037844387076, 1.000000000000000000, 0.8660254037844387076, 1.000000000000000000, 0.8660254037844387076, 1.000000000000000000, 0.8660254037844387076, 1.000000000000000000, 0.8660254037844387076, 1.000000000000000000, 0.8660254037844387076, 1.000000000000000000, 0.8660254037844387076, 1.000000000000000000, 0.9111405409379251807, 0.9401542263054123438),
 ( 1.000000000000000000, 0.8660254037844387076, 1.000000000000000000, 0.8660254037844387076, 1.000000000000000000, 0.8660254037844387076, 1.000000000000000000, 0.8660254037844387076, 1.000000000000000000, 0.8660254037844387076, 1.000000000000000000, 0.8660254037844387076, 1.000000000000000000, 0.8660254037844387076, 1.000000000000000000, 0.8660254037844387076, 1.000000000000000000, 0.8660254037844387076, 1.000000000000000000, 0.8660254037844387076, 1.000000000000000000, 0.8660254037844387076, 1.000000000000000000, 0.8660254037844387076, 1.000000000000000000, 0.8660254037844387076, 1.000000000000000000, 0.8660254037844387076, 1.000000000000000000, 0.8660254037844387076, 1.000000000000000000, 0.8660254037844387076, 1.000000000000000000, 0.8660254037844387076, 1.000000000000000000, 0.8660254037844387076, 1.000000000000000000, 0.8660254037844387076, 1.000000000000000000, 0.8660254037844387076, 1.000000000000000000, 0.8660254037844387076, 1.000000000000000000, 0.8660254037844387076, 1.000000000000000000, 0.8660254037844387076, 1.000000000000000000, 0.8660254037844387076, 1.000000000000000000, 0.8660254037844387076, 1.000000000000000000, 0.8660254037844387076, 1.000000000000000000, 0.9111405409379251807, 0.9401542263054123438) ) ) 
 REPRESENTATION_ITEM ( '' )  SURFACE ( )  );
#10091=CARTESIAN_POINT ( 'NONE',  ( 35.00000000000000000, 126.3079067962035822, 3.846875000614517592 ) ) ;
#10096=DIRECTION ( 'NONE',  ( -0.000000000000000000, -0.000000000000000000, -1.000000000000000000 ) ) ;
#10120=EDGE_CURVE ( 'NONE', #12205, #6711, #6913, .T. ) ;
#10132=CARTESIAN_POINT ( 'NONE',  ( 3.556430356250015024, 90.00000000000000000, 3.903125000614517504 ) ) ;
#10141=CARTESIAN_POINT ( 'NONE',  ( 35.00000000000000711, 53.69209320379639649, 4.015625000614517326 ) ) ;
#10153=CARTESIAN_POINT ( 'NONE',  ( 3.800000000000015365, 90.00000000000000000, 3.200000000000000178 ) ) ;
#10161=CARTESIAN_POINT ( 'NONE',  ( 3.556430356250015024, 90.00000000000000000, 3.509375000614517681 ) ) ;
#10166=FACE_OUTER_BOUND ( 'NONE', #6191, .T. ) ;
#10171=CARTESIAN_POINT ( 'NONE',  ( 36.50000000000001421, 67.79999999999999716, 8.000000000000000000 ) ) ;
#10187=ORIENTED_EDGE ( 'NONE', *, *, #3059, .T. ) ;
#10194=AXIS2_PLACEMENT_3D ( 'NONE', #6782, #950, #12934 ) ;
#10195=ORIENTED_EDGE ( 'NONE', *, *, #5709, .T. ) ;
#10202=CARTESIAN_POINT ( 'NONE',  ( 66.44356964374998142, 108.1539533981018053, 4.615625000614516971 ) ) ;
#10209=CARTESIAN_POINT ( 'NONE',  ( 35.00000000000000711, 53.69209320379639649, 3.565625000614517592 ) ) ;
#10212=( NAMED_UNIT ( * ) PLANE_ANGLE_UNIT ( ) SI_UNIT ( $, .RADIAN. ) );
#10237=B_SPLINE_CURVE_WITH_KNOTS ( 'NONE', 3,
 ( #11859, #10874, #1918, #9891, #12908, #11923, #5963, #10686, #9702, #12719, #7743, #10748, #9412, #3408, #7080, #373, #9350, #906, #6092, #64, #4018, #5112, #8001, #12427, #11984, #2116, #2049, #3031, #6400, #4080, #6028, #4384, #1430, #129, #437, #10023, #8068, #10398 ),
 .UNSPECIFIED., .F., .F.,
 ( 4, 2, 2, 2, 2, 2, 2, 2, 2, 2, 2, 2, 2, 2, 2, 2, 2, 2, 4 ),
 ( 0.000000000000000000, 0.001940799028833090425, 0.003881598057666180851, 0.007763196115332329610, 0.01164479417299847663, 0.01552639223066462452, 0.02328958834599692898, 0.02523038737482999685, 0.02717118640366306126, 0.03105278446132919354, 0.03299358349016226488, 0.03493438251899534663, 0.03881598057666148932, 0.04269757863432762507, 0.04463837766316068600, 0.04657917669199374694, 0.05046077474965985493, 0.05434237280732596292, 0.06210556892265813728 ),
 .UNSPECIFIED. ) ;
#10241=EDGE_CURVE ( 'NONE', #7119, #5860, #7939, .T. ) ;
#10249=VERTEX_POINT ( 'NONE', #7567 ) ;
#10255=PRODUCT_DEFINITION ( 'UNKNOWN', '', #2178, #6205 ) ;
#10265=CARTESIAN_POINT ( 'NONE',  ( 50.72178482187499071, 117.2309300971526937, 2.853125000614517237 ) ) ;
#10276=SURFACE_SIDE_STYLE ('',( #8388 ) ) ;
#10285=VERTEX_POINT ( 'NONE', #2795 ) ;
#10288=CARTESIAN_POINT ( 'NONE',  ( 5.500109330110817041, 100.8955221554261072, 2.999999999999999112 ) ) ;
#10299=CARTESIAN_POINT ( 'NONE',  ( 3.556430356250028790, 71.84604660189818048, 3.096875000614517148 ) ) ;
#10312=ORIENTED_EDGE ( 'NONE', *, *, #7274, .F. ) ;
#10332=ORIENTED_EDGE ( 'NONE', *, *, #12440, .T. ) ;
#10335=CARTESIAN_POINT ( 'NONE',  ( 64.31840935109022439, 100.6710296186405600, 2.661976390793298286 ) ) ;
#10348=ORIENTED_EDGE ( 'NONE', *, *, #4443, .T. ) ;
#10353=CARTESIAN_POINT ( 'NONE',  ( 66.44356964374999563, 90.00000000000000000, 4.184375000614516615 ) ) ;
#10357=CARTESIAN_POINT ( 'NONE',  ( 6.061620567163541473, 102.3095278883966444, 3.000000000000001776 ) ) ;
#10387=ORIENTED_EDGE ( 'NONE', *, *, #6796, .T. ) ;
#10398=CARTESIAN_POINT ( 'NONE',  ( 64.24207199149496716, 100.8784753363798075, 2.999999999999999556 ) ) ;
#10400=CARTESIAN_POINT ( 'NONE',  ( 50.59999999999999432, 117.0199925980744666, 3.162500001229034741 ) ) ;
#10410=FILL_AREA_STYLE ('',( #2438 ) ) ;
#10417=CARTESIAN_POINT ( 'NONE',  ( 66.44356964374999563, 71.84604660189820891, 4.146875000614517859 ) ) ;
#10441=FACE_OUTER_BOUND ( 'NONE', #3951, .T. ) ;
#10464=CARTESIAN_POINT ( 'NONE',  ( 50.60000000000001563, 62.98000740192552627, 3.012500001229034829 ) ) ;
#10468=PLANE ( 'NONE',  #7349 ) ;
#10470=CARTESIAN_POINT ( 'NONE',  ( 44.18196757760600235, 60.16945102741546947, 2.999999999999999112 ) ) ;
#10480=CARTESIAN_POINT ( 'NONE',  ( 35.00000000000000000, 126.3079067962035822, 4.746875000614517504 ) ) ;
#10496=EDGE_CURVE ( 'NONE', #6062, #3535, #3118, .T. ) ;
#10497=ORIENTED_EDGE ( 'NONE', *, *, #4395, .T. ) ;
#10505=CARTESIAN_POINT ( 'NONE',  ( 3.800000000000015365, 90.00000000000000000, 3.762500001229034385 ) ) ;
#10515=CARTESIAN_POINT ( 'NONE',  ( 66.20000000000008811, 108.0133283987162542, 4.362499999999998934 ) ) ;
#10522=CARTESIAN_POINT ( 'NONE',  ( 2.299999999999989608, 90.00000000000000000, 8.000000000000000000 ) ) ;
#10525=VERTEX_POINT ( 'NONE', #8020 ) ;
#10529=CARTESIAN_POINT ( 'NONE',  ( 3.800000000000025135, 71.98667160128366049, 4.250000001229034652 ) ) ;
#10537=CARTESIAN_POINT ( 'NONE',  ( 3.591865698314129496, 91.49237114305354623, 2.999999999999999556 ) ) ;
#10549=CARTESIAN_POINT ( 'NONE',  ( 50.72178482187499071, 117.2309300971526937, 2.909375000614517148 ) ) ;
#10569=ORIENTED_EDGE ( 'NONE', *, *, #8751, .F. ) ;
#10570=CARTESIAN_POINT ( 'NONE',  ( 3.800000000000015365, 90.00000000000000000, 4.549999999999999822 ) ) ;
#10572=ORIENTED_EDGE ( 'NONE', *, *, #8483, .F. ) ;
#10574=LINE ( 'NONE', #4555, #12834 ) ;
#10588=CARTESIAN_POINT ( 'NONE',  ( 66.19999999999988916, 71.98667160128361786, 3.950000001229034829 ) ) ;
#10597=CARTESIAN_POINT ( 'NONE',  ( 50.60000000000001563, 62.98000740192552627, 3.462500001229034563 ) ) ;
#10612=EDGE_LOOP ( 'NONE', ( #8713, #5399, #10387, #5178 ) ) ;
#10613=CARTESIAN_POINT ( 'NONE',  ( 35.00000000000000711, 53.69209320379640360, 3.171875000614517326 ) ) ;
#10628=CARTESIAN_POINT ( 'NONE',  ( 66.20000000000004547, 108.0133283987162969, 3.575000001229034385 ) ) ;
#10634=DIRECTION ( 'NONE',  ( -0.8660254037844400399, 0.000000000000000000, -0.4999999999999975575 ) ) ;
#10648=CARTESIAN_POINT ( 'NONE',  ( 66.19999999999998863, 90.00000000000000000, 3.987500001229034030 ) ) ;
#10664=DIRECTION ( 'NONE',  ( -0.000000000000000000, -0.000000000000000000, -1.000000000000000000 ) ) ;
#10666=( BOUNDED_CURVE ( )  B_SPLINE_CURVE ( 2, ( #1242, #7196, #12103, #8055, #3151, #10010, #2164 ),
 .UNSPECIFIED., .F., .T. ) 
 B_SPLINE_CURVE_WITH_KNOTS ( ( 3, 2, 2, 3 ),
 ( 0.5000000000000001110, 0.5333333333333334370, 0.5666666666666666519, 0.5999999999999999778 ),
 .UNSPECIFIED. ) 
 CURVE ( )  GEOMETRIC_REPRESENTATION_ITEM ( )  RATIONAL_B_SPLINE_CURVE ( ( 0.9999999999999995559, 0.8660254037844391517, 1.000000000000000000, 0.8660254037844387076, 1.000000000000000000, 0.8660254037844387076, 1.000000000000000000 ) ) 
 REPRESENTATION_ITEM ( '' )  );
#10674=CARTESIAN_POINT ( 'NONE',  ( 50.72178482187499071, 117.2309300971526937, 3.303125000614517415 ) ) ;
#10686=CARTESIAN_POINT ( 'NONE',  ( 20.90786924106107847, 118.1001848103160512, 2.999999999999999112 ) ) ;
#10692=CARTESIAN_POINT ( 'NONE',  ( 35.00000000000000000, 126.0266567974326222, 3.087499999999999911 ) ) ;
#10702=CARTESIAN_POINT ( 'NONE',  ( 3.556430356250014579, 108.1539533981018053, 4.371875000614516615 ) ) ;
#10710=EDGE_CURVE ( 'NONE', #7786, #6465, #5236, .T. ) ;
#10723=CARTESIAN_POINT ( 'NONE',  ( 3.759352622210971440, 86.36930750081523911, 3.000000000000000888 ) ) ;
#10743=CARTESIAN_POINT ( 'NONE',  ( 35.00000000000000711, 53.97334320256736362, 4.325000001229033941 ) ) ;
#10748=CARTESIAN_POINT ( 'NONE',  ( 29.40717483660827014, 120.9786552847847361, 2.999999999999999112 ) ) ;
#10751=DIRECTION ( 'NONE',  ( 0.000000000000000000, -0.000000000000000000, -1.000000000000000000 ) ) ;
#10754=CARTESIAN_POINT ( 'NONE',  ( 50.60000000000001563, 62.98000740192552627, 4.700000000000000178 ) ) ;
#10761=EDGE_CURVE ( 'NONE', #3535, #10795, #1333, .T. ) ;
#10769=CARTESIAN_POINT ( 'NONE',  ( 3.556430356250014579, 108.1539533981018053, 3.921875000614517326 ) ) ;
#10785=VERTEX_POINT ( 'NONE', #5653 ) ;
#10789=STYLED_ITEM('',(#12988),#3386);
#10795=VERTEX_POINT ( 'NONE', #1601 ) ;
#10801=CARTESIAN_POINT ( 'NONE',  ( 19.27821517812503060, 62.76906990284727783, 3.528125000614517059 ) ) ;
#10804=CARTESIAN_POINT ( 'NONE',  ( 67.70000000000001705, 90.00000000000000000, 3.000000000000000000 ) ) ;
#10808=LINE ( 'NONE', #1851, #1445 ) ;
#10819=CARTESIAN_POINT ( 'NONE',  ( 3.800000000000025135, 71.98667160128366049, 3.687500000000000888 ) ) ;
#10831=CARTESIAN_POINT ( 'NONE',  ( 3.556430356250014579, 108.1539533981018053, 4.821875000614516793 ) ) ;
#10856=DIRECTION ( 'NONE',  ( 0.000000000000000000, 0.000000000000000000, 1.000000000000000000 ) ) ;
#10860=CARTESIAN_POINT ( 'NONE',  ( 60.63303222545420823, 111.5086687406912347, 2.829484441871016109 ) ) ;
#10868=EDGE_CURVE ( 'NONE', #6711, #10525, #3343, .T. ) ;
#10874=CARTESIAN_POINT ( 'NONE',  ( 14.01316722111233481, 113.4202627883618248, 3.000000000000000444 ) ) ;
#10878=DIRECTION ( 'NONE',  ( 0.000000000000000000, 1.000000000000000000, 0.000000000000000000 ) ) ;
#10881=CARTESIAN_POINT ( 'NONE',  ( 19.27821517812500574, 117.2309300971526937, 4.334375000614516971 ) ) ;
#10891=CARTESIAN_POINT ( 'NONE',  ( 35.00000000000000711, 53.69209320379639649, 4.071875000614516793 ) ) ;
#10914=ADVANCED_FACE ( 'NONE', ( #6759 ), #1666, .T. ) ;
#10920=CARTESIAN_POINT ( 'NONE',  ( 3.556430356250014579, 108.1539533981018053, 4.315625000614517148 ) ) ;
#10924=CARTESIAN_POINT ( 'NONE',  ( 50.72178482187501203, 62.76906990284730625, 3.153125000614517504 ) ) ;
#10930=EDGE_LOOP ( 'NONE', ( #12763, #9369, #9406, #1644 ) ) ;
#10943=CARTESIAN_POINT ( 'NONE',  ( 3.556430356250015024, 90.00000000000000000, 3.059375000614517059 ) ) ;
#10977=VERTEX_POINT ( 'NONE', #12913 ) ;
#10981=CARTESIAN_POINT ( 'NONE',  ( 3.556430356250014579, 108.1539533981018053, 4.315625000614517148 ) ) ;
#10982=( GEOMETRIC_REPRESENTATION_CONTEXT ( 3 ) GLOBAL_UNCERTAINTY_ASSIGNED_CONTEXT ( ( #11159 ) ) GLOBAL_UNIT_ASSIGNED_CONTEXT ( ( #11955, #3796, #11767 ) ) REPRESENTATION_CONTEXT ( 'NONE', 'WORKASPACE' ) );
#10986=CARTESIAN_POINT ( 'NONE',  ( 50.72178482187499071, 117.2309300971526937, 3.303125000614517415 ) ) ;
#10992=AXIS2_PLACEMENT_3D ( 'NONE', #8398, #12381, #12450 ) ;
#10993=CARTESIAN_POINT ( 'NONE',  ( 3.800000000000015365, 90.00000000000000000, 4.100000000000000533 ) ) ;
#10997=LINE ( 'NONE', #11063, #2829 ) ;
#11006=CARTESIAN_POINT ( 'NONE',  ( 35.00000000000000000, 126.3079067962035822, 3.396875000614517415 ) ) ;
#11031=CARTESIAN_POINT ( 'NONE',  ( 35.00000000000000711, 53.97334320256736362, 3.762500000000000178 ) ) ;
#11045=CARTESIAN_POINT ( 'NONE',  ( 35.00000000000000000, 126.3079067962035822, 4.690625000614518036 ) ) ;
#11047=ORIENTED_EDGE ( 'NONE', *, *, #188, .T. ) ;
#11049=EDGE_CURVE ( 'NONE', #12512, #10795, #1859, .T. ) ;
#11052=CARTESIAN_POINT ( 'NONE',  ( 35.00000000000000711, 53.69209320379639649, 3.115625000614517415 ) ) ;
#11057=CARTESIAN_POINT ( 'NONE',  ( 35.00000000000000711, 53.97334320256736362, 4.212500000000000355 ) ) ;
#11063=CARTESIAN_POINT ( 'NONE',  ( 66.20000000000000284, 90.00000000000000000, 6.000000000000000000 ) ) ;
#11068=EDGE_LOOP ( 'NONE', ( #7788, #12373, #4661, #11378, #11753, #4421 ) ) ;
#11072=CARTESIAN_POINT ( 'NONE',  ( 50.72178482187499071, 117.2309300971526937, 4.259375000614517681 ) ) ;
#11076=( BOUNDED_SURFACE ( )  B_SPLINE_SURFACE ( 1, 2, ( 
 ( #1649, #5638, #9500, #10480, #11326, #9630, #5504, #8651, #3424, #5371, #4662, #1515, #7602, #1584, #6354, #2508, #12377, #8591, #10353, #10417, #391, #12581, #3689, #9368, #525, #7472, #9566, #12513, #3557, #7538, #2444, #5572, #6417, #3622, #11591, #3492, #591, #12646, #2640, #4598, #6614, #11525, #4403, #8394, #656, #10613, #2571, #6549, #8458, #9431, #4464, #7406, #10549, #11393, #455 ),
 ( #11458, #5949, #9494, #2767, #4974, #12828, #2955, #5828, #6807, #7667, #908, #9757, #7790, #10920, #11847, #9947, #4787, #8961, #12706, #975, #4914, #1905, #8776, #11782, #9689, #722, #3877, #1971, #1843, #11654, #5886, #12769, #9878, #8834, #10801, #2704, #12896, #3810, #6678, #4852, #10674, #6936, #2893, #1714, #7858, #9819, #5702, #4727, #11909, #7730, #6872, #3748, #8712, #10860, #783 ) ),
 .UNSPECIFIED., .F., .F., .F. ) 
 B_SPLINE_SURFACE_WITH_KNOTS ( ( 2, 2 ),
 ( 3, 2, 2, 2, 2, 2, 2, 2, 2, 2, 2, 2, 2, 2, 2, 2, 2, 2, 2, 2, 2, 2, 2, 2, 2, 2, 2, 3 ),
 ( 0.000000000000000000, 1.000000000000000000 ),
 ( 0.000000000000000000, 0.03333333333333333287, 0.06666666666666666574, 0.1000000000000000056, 0.1333333333333333315, 0.1666666666666666574, 0.2000000000000000111, 0.2333333333333333370, 0.2666666666666666630, 0.2999999999999999889, 0.3333333333333333148, 0.3666666666666666408, 0.4000000000000000222, 0.4333333333333333481, 0.4666666666666666741, 0.5000000000000000000, 0.5333333333333333259, 0.5666666666666666519, 0.5999999999999999778, 0.6333333333333333037, 0.6666666666666666297, 0.6999999999999999556, 0.7333333333333332815, 0.7666666666666667185, 0.8000000000000000444, 0.8333333333333333703, 0.8666666666666666963, 0.8887752010635167066 ),
 .UNSPECIFIED. ) 
 GEOMETRIC_REPRESENTATION_ITEM ( )  RATIONAL_B_SPLINE_SURFACE ( (
 ( 1.000000000000000000, 0.8660254037844387076, 1.000000000000000000, 0.8660254037844387076, 1.000000000000000000, 0.8660254037844387076, 1.000000000000000000, 0.8660254037844387076, 1.000000000000000000, 0.8660254037844387076, 1.000000000000000000, 0.8660254037844387076, 1.000000000000000000, 0.8660254037844387076, 1.000000000000000000, 0.8660254037844387076, 1.000000000000000000, 0.8660254037844387076, 1.000000000000000000, 0.8660254037844387076, 1.000000000000000000, 0.8660254037844387076, 1.000000000000000000, 0.8660254037844387076, 1.000000000000000000, 0.8660254037844387076, 1.000000000000000000, 0.8660254037844387076, 1.000000000000000000, 0.8660254037844387076, 1.000000000000000000, 0.8660254037844387076, 1.000000000000000000, 0.8660254037844387076, 1.000000000000000000, 0.8660254037844387076, 1.000000000000000000, 0.8660254037844387076, 1.000000000000000000, 0.8660254037844387076, 1.000000000000000000, 0.8660254037844387076, 1.000000000000000000, 0.8660254037844387076, 1.000000000000000000, 0.8660254037844387076, 1.000000000000000000, 0.8660254037844387076, 1.000000000000000000, 0.8660254037844387076, 1.000000000000000000, 0.8660254037844387076, 1.000000000000000000, 0.9111405409379251807, 0.9401542263054123438),
 ( 1.000000000000000000, 0.8660254037844387076, 1.000000000000000000, 0.8660254037844387076, 1.000000000000000000, 0.8660254037844387076, 1.000000000000000000, 0.8660254037844387076, 1.000000000000000000, 0.8660254037844387076, 1.000000000000000000, 0.8660254037844387076, 1.000000000000000000, 0.8660254037844387076, 1.000000000000000000, 0.8660254037844387076, 1.000000000000000000, 0.8660254037844387076, 1.000000000000000000, 0.8660254037844387076, 1.000000000000000000, 0.8660254037844387076, 1.000000000000000000, 0.8660254037844387076, 1.000000000000000000, 0.8660254037844387076, 1.000000000000000000, 0.8660254037844387076, 1.000000000000000000, 0.8660254037844387076, 1.000000000000000000, 0.8660254037844387076, 1.000000000000000000, 0.8660254037844387076, 1.000000000000000000, 0.8660254037844387076, 1.000000000000000000, 0.8660254037844387076, 1.000000000000000000, 0.8660254037844387076, 1.000000000000000000, 0.8660254037844387076, 1.000000000000000000, 0.8660254037844387076, 1.000000000000000000, 0.8660254037844387076, 1.000000000000000000, 0.8660254037844387076, 1.000000000000000000, 0.8660254037844387076, 1.000000000000000000, 0.8660254037844387076, 1.000000000000000000, 0.9111405409379251807, 0.9401542263054123438) ) ) 
 REPRESENTATION_ITEM ( '' )  SURFACE ( )  );
#11089=CARTESIAN_POINT ( 'NONE',  ( 3.800000000000015365, 90.00000000000000000, 4.212500001229034119 ) ) ;
#11092=ORIENTED_EDGE ( 'NONE', *, *, #10761, .F. ) ;
#11111=CARTESIAN_POINT ( 'NONE',  ( 19.40000000000000924, 117.0199925980744666, 4.587500001229034119 ) ) ;
#11117=CARTESIAN_POINT ( 'NONE',  ( 3.556430356250015024, 90.00000000000000000, 3.453125000614517770 ) ) ;
#11135=CARTESIAN_POINT ( 'NONE',  ( 50.72178482187501203, 62.76906990284730625, 4.559375000614517504 ) ) ;
#11139=ADVANCED_FACE ( 'NONE', ( #3495 ), #2379, .T. ) ;
#11159=UNCERTAINTY_MEASURE_WITH_UNIT (LENGTH_MEASURE( 1.000000000000000082E-05 ), #11955, 'distance_accuracy_value', 'NONE');
#11163=DIRECTION ( 'NONE',  ( 1.000000000000000000, 0.000000000000000000, -0.000000000000000000 ) ) ;
#11180=CARTESIAN_POINT ( 'NONE',  ( 35.00000000000000711, 53.97334320256736362, 4.325000001229033941 ) ) ;
#11190=CARTESIAN_POINT ( 'NONE',  ( 66.44356964374998142, 108.1539533981018053, 4.165625000614516793 ) ) ;
#11223=FACE_OUTER_BOUND ( 'NONE', #1297, .T. ) ;
#11228=LINE ( 'NONE', #2146, #6477 ) ;
#11233=CYLINDRICAL_SURFACE ( 'NONE', #5559, 31.19999999999999929 ) ;
#11246=CARTESIAN_POINT ( 'NONE',  ( 19.27821517812503060, 62.76906990284727783, 3.528125000614517059 ) ) ;
#11252=DIRECTION ( 'NONE',  ( 0.000000000000000000, 0.000000000000000000, 1.000000000000000000 ) ) ;
#11259=ORIENTED_EDGE ( 'NONE', *, *, #1077, .T. ) ;
#11275=( BOUNDED_CURVE ( )  B_SPLINE_CURVE ( 2, ( #9727, #10588, #12681, #3720, #6457, #8430, #7703 ),
 .UNSPECIFIED., .F., .F. ) 
 B_SPLINE_CURVE_WITH_KNOTS ( ( 3, 2, 2, 3 ),
 ( 0.3000000000000002109, 0.3333333333333334259, 0.3666666666666666963, 0.3999999999999999667 ),
 .UNSPECIFIED. ) 
 CURVE ( )  GEOMETRIC_REPRESENTATION_ITEM ( )  RATIONAL_B_SPLINE_CURVE ( ( 0.9999999999999991118, 0.8660254037844395958, 1.000000000000000000, 0.8660254037844387076, 1.000000000000000000, 0.8660254037844389297, 0.9999999999999997780 ) ) 
 REPRESENTATION_ITEM ( '' )  );
#11309=CARTESIAN_POINT ( 'NONE',  ( 66.20000000000000284, 71.98667160128370313, 3.500000001229034208 ) ) ;
#11324=CARTESIAN_POINT ( 'NONE',  ( 64.24207199149496716, 100.8784753363798075, 2.999999999999999556 ) ) ;
#11326=CARTESIAN_POINT ( 'NONE',  ( 50.72178482187499071, 117.2309300971526937, 4.709375000614516971 ) ) ;
#11337=DIRECTION ( 'NONE',  ( -0.000000000000000000, -0.000000000000000000, -1.000000000000000000 ) ) ;
#11374=CARTESIAN_POINT ( 'NONE',  ( 19.40000000000002700, 62.98000740192551206, 4.287500001229034297 ) ) ;
#11378=ORIENTED_EDGE ( 'NONE', *, *, #9329, .T. ) ;
#11386=PRESENTATION_STYLE_ASSIGNMENT (( #1442 ) ) ;
#11393=CARTESIAN_POINT ( 'NONE',  ( 60.63303222545420823, 111.5086687406912347, 2.885734441871016021 ) ) ;
#11397=CARTESIAN_POINT ( 'NONE',  ( 5.680405782532357506, 101.3717050593596127, 3.000000000000001776 ) ) ;
#11412=ORIENTED_EDGE ( 'NONE', *, *, #2957, .F. ) ;
#11415=ORIENTED_EDGE ( 'NONE', *, *, #6826, .T. ) ;
#11417=CYLINDRICAL_SURFACE ( 'NONE', #12210, 32.70000000000000284 ) ;
#11419=LINE ( 'NONE', #11551, #3845 ) ;
#11420=VERTEX_POINT ( 'NONE', #12771 ) ;
#11440=CARTESIAN_POINT ( 'NONE',  ( 66.20000000000005969, 108.0133283987162685, 4.475000001229034297 ) ) ;
#11454=EDGE_CURVE ( 'NONE', #10285, #10785, #11785, .T. ) ;
#11458=CARTESIAN_POINT ( 'NONE',  ( 3.556430356250015024, 90.00000000000000000, 4.803125000614516971 ) ) ;
#11475=CARTESIAN_POINT ( 'NONE',  ( 50.59999999999999432, 117.0199925980744666, 3.612500001229034474 ) ) ;
#11494=VERTEX_POINT ( 'NONE', #10804 ) ;
#11501=( BOUNDED_CURVE ( )  B_SPLINE_CURVE ( 2, ( #754, #10831, #7956, #9787, #4945, #1935, #1874, #7760, #6710, #4756, #9849, #2006, #5006, #10702, #877, #1743, #8742, #4881, #12864, #12738, #2924, #10891, #11749, #6776, #4819, #10769, #815, #8805, #3909, #8215, #3317, #7163, #6309, #345, #3119, #5328, #1073, #277, #4295, #7297, #8021, #8152, #10042, #5065, #4230, #2333, #2204, #10299, #6246, #5134, #2271 ),
 .UNSPECIFIED., .F., .F. ) 
 B_SPLINE_CURVE_WITH_KNOTS ( ( 3, 2, 2, 2, 2, 2, 2, 2, 2, 2, 2, 2, 2, 2, 2, 2, 2, 2, 2, 2, 2, 2, 2, 2, 2, 3 ),
 ( 0.000000000000000000, 0.03333333333333333287, 0.06666666666666666574, 0.1000000000000000056, 0.1333333333333333315, 0.1666666666666666574, 0.2000000000000000111, 0.2333333333333333370, 0.2666666666666666630, 0.2999999999999999889, 0.3333333333333333148, 0.3666666666666666408, 0.4000000000000000222, 0.4333333333333333481, 0.4666666666666666741, 0.5000000000000000000, 0.5333333333333333259, 0.5666666666666666519, 0.5999999999999999778, 0.6333333333333333037, 0.6666666666666666297, 0.6999999999999999556, 0.7333333333333332815, 0.7666666666666667185, 0.8000000000000000444, 0.8259392087116486092 ),
 .UNSPECIFIED. ) 
 CURVE ( )  GEOMETRIC_REPRESENTATION_ITEM ( )  RATIONAL_B_SPLINE_CURVE ( ( 1.000000000000000000, 0.8660254037844387076, 1.000000000000000000, 0.8660254037844387076, 1.000000000000000000, 0.8660254037844387076, 1.000000000000000000, 0.8660254037844387076, 1.000000000000000000, 0.8660254037844387076, 1.000000000000000000, 0.8660254037844387076, 1.000000000000000000, 0.8660254037844387076, 1.000000000000000000, 0.8660254037844387076, 1.000000000000000000, 0.8660254037844387076, 1.000000000000000000, 0.8660254037844387076, 1.000000000000000000, 0.8660254037844387076, 1.000000000000000000, 0.8660254037844387076, 1.000000000000000000, 0.8660254037844387076, 1.000000000000000000, 0.8660254037844387076, 1.000000000000000000, 0.8660254037844387076, 1.000000000000000000, 0.8660254037844387076, 1.000000000000000000, 0.8660254037844387076, 1.000000000000000000, 0.8660254037844387076, 1.000000000000000000, 0.8660254037844387076, 1.000000000000000000, 0.8660254037844387076, 1.000000000000000000, 0.8660254037844387076, 1.000000000000000000, 0.8660254037844387076, 1.000000000000000000, 0.8660254037844387076, 1.000000000000000000, 0.8660254037844387076, 1.000000000000000000, 0.8957441496011714355, 0.9537471549766802781 ) ) 
 REPRESENTATION_ITEM ( '' )  );
#11506=CARTESIAN_POINT ( 'NONE',  ( 35.00000000000000000, 126.0266567974326222, 4.100000001229034297 ) ) ;
#11513=DIRECTION ( 'NONE',  ( 0.000000000000000000, 0.000000000000000000, -1.000000000000000000 ) ) ;
#11519=AXIS2_PLACEMENT_3D ( 'NONE', #3221, #7134, #3414 ) ;
#11525=CARTESIAN_POINT ( 'NONE',  ( 66.44356964374998142, 108.1539533981018053, 3.321875000614517237 ) ) ;
#11532=DIRECTION ( 'NONE',  ( -1.000000000000000000, 0.000000000000000000, 0.000000000000000000 ) ) ;
#11543=CARTESIAN_POINT ( 'NONE',  ( 66.19999999999998863, 90.00000000000000000, 3.425000000000000266 ) ) ;
#11551=CARTESIAN_POINT ( 'NONE',  ( 3.678215178125014972, 90.00000000000000000, 4.929687500307258219 ) ) ;
#11558=ORIENTED_EDGE ( 'NONE', *, *, #7675, .F. ) ;
#11566=STYLED_ITEM ( 'NONE', ( #11386 ), #5287 ) ;
#11573=CARTESIAN_POINT ( 'NONE',  ( 50.59999999999999432, 117.0199925980744666, 4.062500001229034652 ) ) ;
#11574=VERTEX_POINT ( 'NONE', #2958 ) ;
#11580=CARTESIAN_POINT ( 'NONE',  ( 18.38891503675719008, 63.42664337523432039, 3.000000000000000888 ) ) ;
#11583=AXIS2_PLACEMENT_3D ( 'NONE', #11679, #12603, #748 ) ;
#11585=EDGE_CURVE ( 'NONE', #6465, #7786, #6297, .T. ) ;
#11588=CARTESIAN_POINT ( 'NONE',  ( 35.00000000000000000, 126.0266567974326222, 3.200000001229034385 ) ) ;
#11591=CARTESIAN_POINT ( 'NONE',  ( 19.27821517812503060, 62.76906990284727783, 3.584375000614516971 ) ) ;
#11608=CARTESIAN_POINT ( 'NONE',  ( 3.800000000000015810, 108.0133283987162969, 3.612500000000000711 ) ) ;
#11613=CARTESIAN_POINT ( 'NONE',  ( 3.800000000000025135, 71.98667160128366049, 4.587500000000001243 ) ) ;
#11618=FACE_OUTER_BOUND ( 'NONE', #6082, .T. ) ;
#11619=VERTEX_POINT ( 'NONE', #3354 ) ;
#11626=DIRECTION ( 'NONE',  ( -0.000000000000000000, -1.000000000000000000, -0.000000000000000000 ) ) ;
#11642=DIRECTION ( 'NONE',  ( -1.000000000000000000, 0.000000000000000000, 0.000000000000000000 ) ) ;
#11645=CARTESIAN_POINT ( 'NONE',  ( 13.83140072625826811, 66.88874552888529479, 3.000000000000000888 ) ) ;
#11646=CARTESIAN_POINT ( 'NONE',  ( 19.40000000000002700, 62.98000740192551206, 3.275000000000000355 ) ) ;
#11648=ADVANCED_FACE ( 'NONE', ( #9358 ), #12106, .F. ) ;
#11652=CARTESIAN_POINT ( 'NONE',  ( 3.800000000000015810, 108.0133283987162969, 3.275000001229034563 ) ) ;
#11654=CARTESIAN_POINT ( 'NONE',  ( 66.44356964374998142, 108.1539533981018053, 3.715625000614517948 ) ) ;
#11669=CARTESIAN_POINT ( 'NONE',  ( 35.00000000000000000, 126.0266567974326222, 3.537499999999999645 ) ) ;
#11675=CARTESIAN_POINT ( 'NONE',  ( 3.800000000000015365, 90.00000000000000000, 3.200000000000000178 ) ) ;
#11679=CARTESIAN_POINT ( 'NONE',  ( 3.556430356250015024, 90.00000000000000000, 4.831250000614517148 ) ) ;
#11680=FACE_BOUND ( 'NONE', #3466, .T. ) ;
#11687=CARTESIAN_POINT ( 'NONE',  ( 33.50000000000000711, 67.79999999999999716, 6.000000000000000000 ) ) ;
#11708=CARTESIAN_POINT ( 'NONE',  ( 5.604701438244304335, 78.90188256379346399, 2.999999999999998668 ) ) ;
#11721=CARTESIAN_POINT ( 'NONE',  ( 3.800000000000015365, 90.00000000000000000, 4.100000000000000533 ) ) ;
#11736=CARTESIAN_POINT ( 'NONE',  ( 3.800000000000015365, 108.0133283987163111, 4.962499999999999467 ) ) ;
#11742=EDGE_CURVE ( 'NONE', #6062, #12512, #9485, .T. ) ;
#11749=CARTESIAN_POINT ( 'NONE',  ( 19.27821517812503060, 62.76906990284727783, 4.034375000614517148 ) ) ;
#11753=ORIENTED_EDGE ( 'NONE', *, *, #8141, .F. ) ;
#11754=ADVANCED_FACE ( 'NONE', ( #9555 ), #10468, .T. ) ;
#11756=FACE_OUTER_BOUND ( 'NONE', #6163, .T. ) ;
#11767=( NAMED_UNIT ( * ) SI_UNIT ( $, .STERADIAN. ) SOLID_ANGLE_UNIT ( ) );
#11782=CARTESIAN_POINT ( 'NONE',  ( 3.556430356250028790, 71.84604660189818048, 3.940625000614518036 ) ) ;
#11785=LINE ( 'NONE', #4916, #8180 ) ;
#11803=CARTESIAN_POINT ( 'NONE',  ( 66.20000000000008811, 108.0133283987162542, 3.462499999999999467 ) ) ;
#11806=CARTESIAN_POINT ( 'NONE',  ( 19.40000000000002700, 62.98000740192551206, 4.625000000000000000 ) ) ;
#11847=CARTESIAN_POINT ( 'NONE',  ( 19.27821517812500574, 117.2309300971526937, 4.278125000614516615 ) ) ;
#11850=CARTESIAN_POINT ( 'NONE',  ( 35.00000000000000000, 126.0266567974326222, 3.987500000000000266 ) ) ;
#11855=ADVANCED_FACE ( 'NONE', ( #9931 ), #6793, .F. ) ;
#11859=CARTESIAN_POINT ( 'NONE',  ( 13.53859087060910404, 112.9805567844265539, 2.999999999999999112 ) ) ;
#11867=CARTESIAN_POINT ( 'NONE',  ( 66.44356964374998142, 108.1539533981018053, 4.671875000614516438 ) ) ;
#11889=DIRECTION ( 'NONE',  ( 1.000000000000000000, 0.000000000000000000, 0.000000000000000000 ) ) ;
#11893=ORIENTED_EDGE ( 'NONE', *, *, #2283, .T. ) ;
#11909=CARTESIAN_POINT ( 'NONE',  ( 3.556430356250015024, 90.00000000000000000, 3.003125000614517148 ) ) ;
#11923=CARTESIAN_POINT ( 'NONE',  ( 17.58542467432373257, 116.1886173078550542, 3.000000000000001332 ) ) ;
#11932=CARTESIAN_POINT ( 'NONE',  ( 35.00000000000000711, 53.69209320379640360, 3.171875000614517326 ) ) ;
#11955=( LENGTH_UNIT ( ) NAMED_UNIT ( * ) SI_UNIT ( .MILLI., .METRE. ) );
#11975=CARTESIAN_POINT ( 'NONE',  ( 3.556430356250015024, 90.00000000000000000, 3.903125000614517504 ) ) ;
#11984=CARTESIAN_POINT ( 'NONE',  ( 48.20636397115843153, 118.4025818652226860, 3.000000000000001776 ) ) ;
#11993=CARTESIAN_POINT ( 'NONE',  ( 35.00000000000000711, 53.69209320379640360, 4.521875000614516971 ) ) ;
#11999=AXIS2_PLACEMENT_3D ( 'NONE', #2790, #12921, #6962 ) ;
#12030=ADVANCED_FACE ( 'NONE', ( #7811 ), #8107, .T. ) ;
#12038=CARTESIAN_POINT ( 'NONE',  ( 19.27821517812500574, 117.2309300971526937, 3.828125000614516882 ) ) ;
#12043=CARTESIAN_POINT ( 'NONE',  ( 66.44356964374999563, 90.00000000000000000, 4.128125000614517148 ) ) ;
#12059=UNCERTAINTY_MEASURE_WITH_UNIT (LENGTH_MEASURE( 1.000000000000000082E-05 ), #6222, 'distance_accuracy_value', 'NONE');
#12062=CARTESIAN_POINT ( 'NONE',  ( 3.556430356250015024, 90.00000000000000000, 3.959375000614517415 ) ) ;
#12088=CARTESIAN_POINT ( 'NONE',  ( 36.50000000000001421, 79.80000000000001137, 8.000000000000000000 ) ) ;
#12091=ORIENTED_EDGE ( 'NONE', *, *, #9064, .T. ) ;
#12099=CARTESIAN_POINT ( 'NONE',  ( 19.27821517812503060, 62.76906990284727783, 4.428125000614516971 ) ) ;
#12100=VECTOR ( 'NONE', #1394, 1000.000000000000000 ) ;
#12103=CARTESIAN_POINT ( 'NONE',  ( 50.60000000000001563, 62.98000740192552627, 3.462500001229034563 ) ) ;
#12106=CYLINDRICAL_SURFACE ( 'NONE', #11519, 31.19999999999999929 ) ;
#12107=CARTESIAN_POINT ( 'NONE',  ( 3.556430356250015024, 90.00000000000000000, 4.803125000614516971 ) ) ;
#12129=CARTESIAN_POINT ( 'NONE',  ( 3.556430356250028790, 71.84604660189818048, 3.096875000614517592 ) ) ;
#12154=FACE_OUTER_BOUND ( 'NONE', #3588, .T. ) ;
#12168=CARTESIAN_POINT ( 'NONE',  ( 66.20000000000000284, 71.98667160128370313, 4.400000001229034119 ) ) ;
#12174=CARTESIAN_POINT ( 'NONE',  ( 50.72178482187499071, 117.2309300971526937, 3.753125000614517592 ) ) ;
#12178=( NAMED_UNIT ( * ) SI_UNIT ( $, .STERADIAN. ) SOLID_ANGLE_UNIT ( ) );
#12182=EDGE_CURVE ( 'NONE', #998, #4984, #10012, .T. ) ;
#12205=VERTEX_POINT ( 'NONE', #7136 ) ;
#12210=AXIS2_PLACEMENT_3D ( 'NONE', #5661, #12471, #5460 ) ;
#12235=CARTESIAN_POINT ( 'NONE',  ( 35.00000000000000000, 126.3079067962035822, 2.890625000614516882 ) ) ;
#12244=CARTESIAN_POINT ( 'NONE',  ( 66.19999999999998863, 90.00000000000000000, 3.537500001229034297 ) ) ;
#12252=CARTESIAN_POINT ( 'NONE',  ( 19.40000000000000924, 117.0199925980744666, 3.125000000000000000 ) ) ;
#12289=ORIENTED_EDGE ( 'NONE', *, *, #1409, .F. ) ;
#12291=CARTESIAN_POINT ( 'NONE',  ( 36.50000000000001421, 67.79999999999999716, 8.000000000000000000 ) ) ;
#12298=CARTESIAN_POINT ( 'NONE',  ( 66.44356964374999563, 90.00000000000000000, 3.678125000614516971 ) ) ;
#12353=VERTEX_POINT ( 'NONE', #12244 ) ;
#12363=CARTESIAN_POINT ( 'NONE',  ( 50.59999999999999432, 117.0199925980744666, 3.612500001229034474 ) ) ;
#12373=ORIENTED_EDGE ( 'NONE', *, *, #9583, .F. ) ;
#12377=CARTESIAN_POINT ( 'NONE',  ( 50.72178482187499071, 117.2309300971526937, 4.259375000614517681 ) ) ;
#12381=DIRECTION ( 'NONE',  ( 0.000000000000000000, 0.000000000000000000, 1.000000000000000000 ) ) ;
#12401=PLANE ( 'NONE',  #11583 ) ;
#12419=ORIENTED_EDGE ( 'NONE', *, *, #10120, .F. ) ;
#12424=( BOUNDED_CURVE ( )  B_SPLINE_CURVE ( 2, ( #6444, #1476, #9828, #12540, #5461, #8485, #856 ),
 .UNSPECIFIED., .F., .F. ) 
 B_SPLINE_CURVE_WITH_KNOTS ( ( 3, 2, 2, 3 ),
 ( 0.1000000000000001860, 0.1333333333333334425, 0.1666666666666666852, 0.2000000000000000111 ),
 .UNSPECIFIED. ) 
 CURVE ( )  GEOMETRIC_REPRESENTATION_ITEM ( )  RATIONAL_B_SPLINE_CURVE ( ( 0.9999999999999992228, 0.8660254037844394848, 1.000000000000000000, 0.8660254037844387076, 1.000000000000000000, 0.8660254037844388186, 0.9999999999999998890 ) ) 
 REPRESENTATION_ITEM ( '' )  );
#12427=CARTESIAN_POINT ( 'NONE',  ( 47.03610297002379781, 118.9238557598572896, 3.000000000000000444 ) ) ;
#12429=CARTESIAN_POINT ( 'NONE',  ( 3.800000000000015365, 90.00000000000000000, 4.662500001229034297 ) ) ;
#12440=EDGE_CURVE ( 'NONE', #12799, #12605, #9671, .T. ) ;
#12450=DIRECTION ( 'NONE',  ( 1.000000000000000000, 0.000000000000000000, 0.000000000000000000 ) ) ;
#12459=CARTESIAN_POINT ( 'NONE',  ( 66.20000000000000284, 90.00000000000000000, 3.000000000000000000 ) ) ;
#12471=DIRECTION ( 'NONE',  ( -0.000000000000000000, -0.000000000000000000, -1.000000000000000000 ) ) ;
#12484=LINE ( 'NONE', #11687, #5365 ) ;
#12512=VERTEX_POINT ( 'NONE', #966 ) ;
#12513=CARTESIAN_POINT ( 'NONE',  ( 35.00000000000000000, 126.3079067962035822, 3.846875000614517592 ) ) ;
#12539=LINE ( 'NONE', #480, #1770 ) ;
#12540=CARTESIAN_POINT ( 'NONE',  ( 35.00000000000000711, 53.97334320256736362, 4.662499999999999645 ) ) ;
#12564=CARTESIAN_POINT ( 'NONE',  ( 60.43447243729646345, 111.3420572890634048, 2.688859442485532991 ) ) ;
#12567=ORIENTED_EDGE ( 'NONE', *, *, #10241, .T. ) ;
#12573=CARTESIAN_POINT ( 'NONE',  ( 8.822182765162120077, 72.71083356296912825, 3.000000000000001776 ) ) ;
#12579=CARTESIAN_POINT ( 'NONE',  ( 66.20000000000008811, 108.0133283987162542, 3.125000001229034208 ) ) ;
#12581=CARTESIAN_POINT ( 'NONE',  ( 35.00000000000000711, 53.69209320379640360, 4.071875000614516793 ) ) ;
#12588=CARTESIAN_POINT ( 'NONE',  ( 66.20000000000000284, 90.00000000000000000, 6.000000000000000000 ) ) ;
#12597=CARTESIAN_POINT ( 'NONE',  ( 19.40000000000000924, 117.0199925980744666, 4.924999999999999822 ) ) ;
#12603=DIRECTION ( 'NONE',  ( 0.000000000000000000, -1.000000000000000000, 0.000000000000000000 ) ) ;
#12604=PLANE ( 'NONE',  #490 ) ;
#12605=VERTEX_POINT ( 'NONE', #3993 ) ;
#12613=CARTESIAN_POINT ( 'NONE',  ( 66.19999999999998863, 90.00000000000000000, 4.325000000000000178 ) ) ;
#12627=CARTESIAN_POINT ( 'NONE',  ( 19.40000000000002700, 62.98000740192551206, 3.387500001229033941 ) ) ;
#12628=VERTEX_POINT ( 'NONE', #234 ) ;
#12634=CARTESIAN_POINT ( 'NONE',  ( 27.76326592528804582, 59.46858721371755507, 3.000000000000000000 ) ) ;
#12646=CARTESIAN_POINT ( 'NONE',  ( 3.556430356250014579, 108.1539533981018053, 3.471875000614516704 ) ) ;
#12681=CARTESIAN_POINT ( 'NONE',  ( 50.60000000000001563, 62.98000740192552627, 3.912500001229034297 ) ) ;
#12706=CARTESIAN_POINT ( 'NONE',  ( 66.44356964374999563, 90.00000000000000000, 4.128125000614517148 ) ) ;
#12719=CARTESIAN_POINT ( 'NONE',  ( 24.44860983802972498, 119.5968892347202654, 2.999999999999997780 ) ) ;
#12726=CARTESIAN_POINT ( 'NONE',  ( 3.800000000000015365, 108.0133283987163111, 3.612500000000000711 ) ) ;
#12738=CARTESIAN_POINT ( 'NONE',  ( 66.44356964375000985, 71.84604660189820891, 4.146875000614517859 ) ) ;
#12748=AXIS2_PLACEMENT_3D ( 'NONE', #8166, #4178, #11163 ) ;
#12763=ORIENTED_EDGE ( 'NONE', *, *, #6720, .F. ) ;
#12769=CARTESIAN_POINT ( 'NONE',  ( 66.44356964374999563, 71.84604660189820891, 3.640625000614517326 ) ) ;
#12771=CARTESIAN_POINT ( 'NONE',  ( 13.53859087060910404, 112.9805567844265539, 2.999999999999999112 ) ) ;
#12787=CARTESIAN_POINT ( 'NONE',  ( 66.19999999999997442, 108.0133283987163253, 4.362499999999999822 ) ) ;
#12789=VERTEX_POINT ( 'NONE', #8688 ) ;
#12796=EDGE_CURVE ( 'NONE', #7089, #451, #11275, .T. ) ;
#12799=VERTEX_POINT ( 'NONE', #564 ) ;
#12822=DIRECTION ( 'NONE',  ( 1.000000000000000000, 0.000000000000000000, 0.000000000000000000 ) ) ;
#12828=CARTESIAN_POINT ( 'NONE',  ( 66.44356964374998142, 108.1539533981018053, 4.615625000614516971 ) ) ;
#12834=VECTOR ( 'NONE', #4622, 1000.000000000000000 ) ;
#12852=CARTESIAN_POINT ( 'NONE',  ( 35.00000000000000711, 53.97334320256736362, 3.312500000000000000 ) ) ;
#12864=CARTESIAN_POINT ( 'NONE',  ( 66.44356964374999563, 90.00000000000000000, 4.184375000614516615 ) ) ;
#12896=CARTESIAN_POINT ( 'NONE',  ( 3.556430356250015024, 90.00000000000000000, 3.453125000614517770 ) ) ;
#12899=CARTESIAN_POINT ( 'NONE',  ( 19.40000000000000924, 117.0199925980744666, 4.025000000000000355 ) ) ;
#12901=CARTESIAN_POINT ( 'NONE',  ( 3.800000000000015810, 108.0133283987162969, 4.962499999999999467 ) ) ;
#12908=CARTESIAN_POINT ( 'NONE',  ( 16.01593418524656798, 115.0585008649344019, 3.000000000000000888 ) ) ;
#12913=CARTESIAN_POINT ( 'NONE',  ( 33.50000000000000711, 79.80000000000001137, 6.000000000000000000 ) ) ;
#12916=CARTESIAN_POINT ( 'NONE',  ( 3.556430356250014579, 108.1539533981018053, 3.471875000614516704 ) ) ;
#12917=CARTESIAN_POINT ( 'NONE',  ( 3.800000000000015365, 90.00000000000000000, 3.200000000000000178 ) ) ;
#12921=DIRECTION ( 'NONE',  ( -0.000000000000000000, -0.000000000000000000, -1.000000000000000000 ) ) ;
#12934=DIRECTION ( 'NONE',  ( 1.000000000000000000, 0.000000000000000000, 0.000000000000000000 ) ) ;
#12982=COLOUR_RGB('Light Blue',0.38,0.62,0.78);
#12983=FILL_AREA_STYLE_COLOUR('',#12982);
#12984=FILL_AREA_STYLE('',(#12983));
#12985=SURFACE_STYLE_FILL_AREA(#12984);
#12986=SURFACE_SIDE_STYLE('',(#12985));
#12987=SURFACE_STYLE_USAGE(.BOTH.,#12986);
#12988=PRESENTATION_STYLE_ASSIGNMENT((#12987));
ENDSEC;
END-ISO-10303-21;
